ISO-10303-21;
HEADER;
FILE_DESCRIPTION (('STEP AP214'),
    '1' );
FILE_NAME ('Cap.step',
    '2026-10-06T14:00:01',
    ( '' ),
    ( '' ),
    'SwSTEP 2.0',
    'SolidWorks 2020',
    '' );
FILE_SCHEMA (( 'AUTOMOTIVE_DESIGN' ));
ENDSEC;

DATA;
#1=ORIENTED_EDGE ( 'NONE', *, *, #26816, .F. ) ;
#16=CARTESIAN_POINT ( 'NONE',  ( -56.67499999999996874, 3.131991715727200307E-15, -1.107867533772800737E-16 ) ) ;
#27=AXIS2_PLACEMENT_3D ( 'NONE', #565, #25255, #22895 ) ;
#44=CARTESIAN_POINT ( 'NONE',  ( -58.09585481156723574, -1.184343223768586473, -3.558065644182725418 ) ) ;
#76=VERTEX_POINT ( 'NONE', #8197 ) ;
#77=CIRCLE ( 'NONE', #6150, 4.800000000000000711 ) ;
#87=FACE_OUTER_BOUND ( 'NONE', #20854, .T. ) ;
#89=AXIS2_PLACEMENT_3D ( 'NONE', #15577, #7805, #3067 ) ;
#96=ORIENTED_EDGE ( 'NONE', *, *, #12745, .F. ) ;
#98=CARTESIAN_POINT ( 'NONE',  ( -55.79792740578360366, 3.330682475591789871, 0.6830477631804102723 ) ) ;
#123=ORIENTED_EDGE ( 'NONE', *, *, #26906, .T. ) ;
#143=ORIENTED_EDGE ( 'NONE', *, *, #13652, .F. ) ;
#144=CARTESIAN_POINT ( 'NONE',  ( -59.81249999999997158, 4.108500314926511798, -1.367561758111406567 ) ) ;
#159=EDGE_CURVE ( 'NONE', #28004, #13558, #14466, .T. ) ;
#161=CARTESIAN_POINT ( 'NONE',  ( -56.62499999999997158, 1.184343223768582254, 3.558065644182727638 ) ) ;
#189=DIRECTION ( 'NONE',  ( 0.000000000000000000, -0.2008964009354148594, 0.9796124928211140670 ) ) ;
#206=EDGE_LOOP ( 'NONE', ( #13546, #11977, #21657, #23791 ) ) ;
#210=ORIENTED_EDGE ( 'NONE', *, *, #23024, .T. ) ;
#218=FACE_OUTER_BOUND ( 'NONE', #18883, .T. ) ;
#236=VERTEX_POINT ( 'NONE', #8450 ) ;
#239=CARTESIAN_POINT ( 'NONE',  ( -54.86042740578361077, -0.7887156198831597465, 3.845940847736172952 ) ) ;
#241=CARTESIAN_POINT ( 'NONE',  ( -67.99999999999995737, -0.5554785485864222050, 2.708628542650383331 ) ) ;
#244=ORIENTED_EDGE ( 'NONE', *, *, #10930, .T. ) ;
#288=CARTESIAN_POINT ( 'NONE',  ( -57.93749999999997158, -4.108500314926507357, 1.367561758111406567 ) ) ;
#330=CARTESIAN_POINT ( 'NONE',  ( -55.11042740578361077, 3.725040285533371076, -1.239922660687676315 ) ) ;
#333=VERTEX_POINT ( 'NONE', #21741 ) ;
#338=AXIS2_PLACEMENT_3D ( 'NONE', #16361, #30597, #23665 ) ;
#344=FACE_OUTER_BOUND ( 'NONE', #13767, .T. ) ;
#351=DIRECTION ( 'NONE',  ( 0.000000000000000000, -0.2008964009354143876, 0.9796124928211140670 ) ) ;
#358=CARTESIAN_POINT ( 'NONE',  ( -60.49999999999995737, 1.963826825011730345E-15, 6.704595576490977020E-16 ) ) ;
#378=AXIS2_PLACEMENT_3D ( 'NONE', #1428, #11090, #30545 ) ;
#399=EDGE_CURVE ( 'NONE', #24313, #24734, #20298, .T. ) ;
#403=DIRECTION ( 'NONE',  ( 2.614375865348240525E-16, -0.2008964009354147762, 0.9796124928211140670 ) ) ;
#404=CARTESIAN_POINT ( 'NONE',  ( -59.98542740578359656, -3.725040285533365303, 1.239922660687675871 ) ) ;
#410=CARTESIAN_POINT ( 'NONE',  ( -56.03335481156723574, -4.108500314926509134, 1.367561758111407455 ) ) ;
#417=ORIENTED_EDGE ( 'NONE', *, *, #10614, .T. ) ;
#448=CARTESIAN_POINT ( 'NONE',  ( -60.81249999999997158, -3.238593381231841040, -2.874284765127020247 ) ) ;
#450=CARTESIAN_POINT ( 'NONE',  ( -55.24999999999997868, 3.673546848079180638, 0.7533615035078062849 ) ) ;
#455=DIRECTION ( 'NONE',  ( -1.000000000000000000, -3.054025858079668409E-16, 2.042474015755241579E-16 ) ) ;
#484=DIRECTION ( 'NONE',  ( 0.000000000000000000, -0.2008964009354147762, 0.9796124928211140670 ) ) ;
#515=EDGE_CURVE ( 'NONE', #6742, #24689, #10204, .T. ) ;
#522=SURFACE_STYLE_USAGE ( .BOTH. , #27114 ) ;
#526=ORIENTED_EDGE ( 'NONE', *, *, #3756, .F. ) ;
#531=ORIENTED_EDGE ( 'NONE', *, *, #17069, .T. ) ;
#547=ORIENTED_EDGE ( 'NONE', *, *, #28384, .F. ) ;
#551=DIRECTION ( 'NONE',  ( 1.000000000000000000, 3.054025858079668409E-16, -2.042474015755241579E-16 ) ) ;
#552=CARTESIAN_POINT ( 'NONE',  ( -60.67292740578359656, -3.330682475591783653, -0.6830477631804101613 ) ) ;
#563=CARTESIAN_POINT ( 'NONE',  ( -58.43749999999997158, 0.7533615035078148336, -3.673546848079175309 ) ) ;
#564=ADVANCED_FACE ( 'NONE', ( #964, #8232 ), #9016, .T. ) ;
#565=CARTESIAN_POINT ( 'NONE',  ( -71.49999999999998579, -1.395601618875910821E-15, 2.917180974979867506E-15 ) ) ;
#587=CARTESIAN_POINT ( 'NONE',  ( -54.97085481156724285, 2.489203624310592833, -2.804704140674919799 ) ) ;
#597=CARTESIAN_POINT ( 'NONE',  ( -57.81249999999997158, -3.238593381231840596, -2.874284765127020691 ) ) ;
#614=CARTESIAN_POINT ( 'NONE',  ( -57.77499999999997016, 2.796048871338436190E-15, 1.138853883557972617E-16 ) ) ;
#619=UNCERTAINTY_MEASURE_WITH_UNIT (LENGTH_MEASURE( 1.000000000000000082E-05 ), #17870, 'distance_accuracy_value', 'NONE');
#653=FACE_OUTER_BOUND ( 'NONE', #21981, .T. ) ;
#692=CARTESIAN_POINT ( 'NONE',  ( -60.54999999999995453, 1.948556695721332102E-15, 6.806719277278738347E-16 ) ) ;
#700=CARTESIAN_POINT ( 'NONE',  ( -60.79792740578359656, -2.256877952708263635, 2.542931754211925188 ) ) ;
#709=VERTEX_POINT ( 'NONE', #15006 ) ;
#724=AXIS2_PLACEMENT_3D ( 'NONE', #17106, #455, #19785 ) ;
#732=CARTESIAN_POINT ( 'NONE',  ( -59.29999999999995453, 0.8061685447651361081, 3.512174729956796249 ) ) ;
#741=CARTESIAN_POINT ( 'NONE',  ( -55.09585481156724285, -1.184343223768585807, -3.558065644182726306 ) ) ;
#753=CARTESIAN_POINT ( 'NONE',  ( -58.56249999999997158, -3.238593381231840596, -2.874284765127020691 ) ) ;
#767=EDGE_CURVE ( 'NONE', #15338, #3096, #24468, .T. ) ;
#781=ORIENTED_EDGE ( 'NONE', *, *, #15945, .F. ) ;
#785=ORIENTED_EDGE ( 'NONE', *, *, #10926, .F. ) ;
#788=CARTESIAN_POINT ( 'NONE',  ( -54.73542740578361077, -3.725040285533364859, 1.239922660687674760 ) ) ;
#795=CARTESIAN_POINT ( 'NONE',  ( -59.29999999999999005, -2.918520965380715371, 1.872283793155697706 ) ) ;
#802=AXIS2_PLACEMENT_3D ( 'NONE', #29576, #17728, #17572 ) ;
#821=DIRECTION ( 'NONE',  ( 0.000000000000000000, 0.2008964009354147762, -0.9796124928211140670 ) ) ;
#856=CIRCLE ( 'NONE', #8940, 4.849999999999999645 ) ;
#875=CARTESIAN_POINT ( 'NONE',  ( -59.04792740578360366, -1.073804522883517132, -3.225979517392335350 ) ) ;
#929=CARTESIAN_POINT ( 'NONE',  ( -69.18535533905931345, -0.4248245016402720786, 2.071532327734953327 ) ) ;
#930=DIRECTION ( 'NONE',  ( 0.000000000000000000, -0.2008964009354147484, 0.9796124928211139560 ) ) ;
#932=PRESENTATION_STYLE_ASSIGNMENT (( #20729 ) ) ;
#960=ORIENTED_EDGE ( 'NONE', *, *, #7724, .T. ) ;
#962=DIRECTION ( 'NONE',  ( 2.581436205204234006E-16, -0.9796124928211140670, -0.2008964009354148872 ) ) ;
#963=CARTESIAN_POINT ( 'NONE',  ( -56.86042740578360366, -2.936324665650200672, -2.606018187048497747 ) ) ;
#964=FACE_BOUND ( 'NONE', #10267, .T. ) ;
#979=DIRECTION ( 'NONE',  ( -2.581436205204234499E-16, 0.9796124928211140670, 0.2008964009354147762 ) ) ;
#982=CARTESIAN_POINT ( 'NONE',  ( -54.49999999999997868, 0.7936213912637685164, -3.348412945455685907 ) ) ;
#1005=DIRECTION ( 'NONE',  ( 0.000000000000000000, -0.2008964009354147484, 0.9796124928211139560 ) ) ;
#1009=ADVANCED_FACE ( 'NONE', ( #29077 ), #17212, .F. ) ;
#1031=CARTESIAN_POINT ( 'NONE',  ( -57.29792740578360366, 3.330682475591789871, 0.6830477631804107164 ) ) ;
#1039=EDGE_LOOP ( 'NONE', ( #4960, #20256, #26777, #6675, #14995 ) ) ;
#1042=DIRECTION ( 'NONE',  ( -2.581436205204234499E-16, 0.9796124928211140670, 0.2008964009354147762 ) ) ;
#1055=ADVANCED_FACE ( 'NONE', ( #26855 ), #20353, .F. ) ;
#1068=ORIENTED_EDGE ( 'NONE', *, *, #20852, .T. ) ;
#1074=VERTEX_POINT ( 'NONE', #7387 ) ;
#1108=CARTESIAN_POINT ( 'NONE',  ( -57.04792740578359656, -2.256877952708263635, 2.542931754211924300 ) ) ;
#1113=EDGE_CURVE ( 'NONE', #9750, #11521, #19253, .T. ) ;
#1115=EDGE_LOOP ( 'NONE', ( #13305, #18253, #30377, #417 ) ) ;
#1133=LINE ( 'NONE', #10641, #23637 ) ;
#1153=DIRECTION ( 'NONE',  ( 1.000000000000000000, 3.054025858079668409E-16, -2.042474015755241579E-16 ) ) ;
#1156=CARTESIAN_POINT ( 'NONE',  ( -67.99999999999997158, -0.3264566515200493790, 1.591870300834312690 ) ) ;
#1157=CARTESIAN_POINT ( 'NONE',  ( -57.03335481156722864, 3.238593381231848145, 2.874284765127023356 ) ) ;
#1158=CARTESIAN_POINT ( 'NONE',  ( -54.56249999999997868, 4.108500314926512686, -1.367561758111408121 ) ) ;
#1160=DIRECTION ( 'NONE',  ( 0.000000000000000000, -0.2008964009354147484, 0.9796124928211139560 ) ) ;
#1167=ADVANCED_FACE ( 'NONE', ( #2948, #22279 ), #15613, .T. ) ;
#1184=ADVANCED_FACE ( 'NONE', ( #30156 ), #18158, .F. ) ;
#1195=DIRECTION ( 'NONE',  ( -1.000000000000000000, -3.054025858079668409E-16, 2.042474015755241579E-16 ) ) ;
#1205=CARTESIAN_POINT ( 'NONE',  ( -54.90835481156723574, 4.108500314926515351, -1.367561758111408565 ) ) ;
#1209=DIRECTION ( 'NONE',  ( -2.581436205204234499E-16, 0.9796124928211140670, 0.2008964009354147762 ) ) ;
#1227=CARTESIAN_POINT ( 'NONE',  ( -54.49999999999997868, 0.2900967345938421649, -3.387601494358211340 ) ) ;
#1228=FACE_OUTER_BOUND ( 'NONE', #23026, .T. ) ;
#1229=AXIS2_PLACEMENT_3D ( 'NONE', #9760, #16741, #26063 ) ;
#1248=CARTESIAN_POINT ( 'NONE',  ( -55.53335481156722864, 3.238593381231848145, 2.874284765127022467 ) ) ;
#1250=CARTESIAN_POINT ( 'NONE',  ( -56.42292740578360366, 1.073804522883522239, 3.225979517392336238 ) ) ;
#1261=EDGE_CURVE ( 'NONE', #7998, #29251, #5577, .T. ) ;
#1267=CARTESIAN_POINT ( 'NONE',  ( -54.49999999999996447, 3.524671047264929857, -0.9892662586404576963 ) ) ;
#1317=DIRECTION ( 'NONE',  ( 0.000000000000000000, 0.2008964009354147484, -0.9796124928211139560 ) ) ;
#1363=CARTESIAN_POINT ( 'NONE',  ( -59.06249999999997158, 4.108500314926519792, -1.367561758111384140 ) ) ;
#1369=CARTESIAN_POINT ( 'NONE',  ( -58.84585481156723574, -1.184343223768586473, -3.558065644182725418 ) ) ;
#1381=DIRECTION ( 'NONE',  ( -1.000000000000000000, -3.054025858079668409E-16, 2.042474015755241579E-16 ) ) ;
#1398=DIRECTION ( 'NONE',  ( 1.000000000000000000, 3.054025858079668409E-16, -2.042474015755241579E-16 ) ) ;
#1415=CARTESIAN_POINT ( 'NONE',  ( -56.17292740578360366, -3.330682475591782765, -0.6830477631804111605 ) ) ;
#1418=AXIS2_PLACEMENT_3D ( 'NONE', #9416, #25876, #21459 ) ;
#1428=CARTESIAN_POINT ( 'NONE',  ( -57.72499999999997300, 2.811319000628834039E-15, 1.036730182770210180E-16 ) ) ;
#1459=AXIS2_PLACEMENT_3D ( 'NONE', #5210, #4906, #17574 ) ;
#1477=DIRECTION ( 'NONE',  ( 0.000000000000000000, -0.2008964009354147762, 0.9796124928211140670 ) ) ;
#1508=CIRCLE ( 'NONE', #26289, 2.100000000000000089 ) ;
#1520=ORIENTED_EDGE ( 'NONE', *, *, #16091, .F. ) ;
#1522=CARTESIAN_POINT ( 'NONE',  ( -57.03335481156722864, 3.238593381231848145, 2.874284765127022911 ) ) ;
#1543=CARTESIAN_POINT ( 'NONE',  ( -59.11042740578360366, -2.936324665650199783, -2.606018187048500412 ) ) ;
#1556=ADVANCED_FACE ( 'NONE', ( #28815 ), #8808, .T. ) ;
#1565=CARTESIAN_POINT ( 'NONE',  ( -57.98542740578359656, 2.936324665650206889, 2.606018187048499080 ) ) ;
#1569=DIRECTION ( 'NONE',  ( 1.000000000000000000, 3.054025858079668409E-16, -2.042474015755241579E-16 ) ) ;
#1573=CARTESIAN_POINT ( 'NONE',  ( -57.31249999999996447, -0.7533615035078060629, 3.673546848079176197 ) ) ;
#1601=ORIENTED_EDGE ( 'NONE', *, *, #767, .F. ) ;
#1604=AXIS2_PLACEMENT_3D ( 'NONE', #20605, #27537, #6178 ) ;
#1612=DIRECTION ( 'NONE',  ( 1.000000000000000000, 3.054025858079668409E-16, -2.042474015755241579E-16 ) ) ;
#1628=ADVANCED_FACE ( 'NONE', ( #26756, #27209 ), #29279, .F. ) ;
#1648=FACE_OUTER_BOUND ( 'NONE', #24289, .T. ) ;
#1653=DIRECTION ( 'NONE',  ( 1.000000000000000000, 3.054025858079668409E-16, -2.042474015755241579E-16 ) ) ;
#1654=CARTESIAN_POINT ( 'NONE',  ( -59.12486116251333357, -1.737685414808515905, 3.471684241605564658 ) ) ;
#1661=ADVANCED_FACE ( 'NONE', ( #19471 ), #2369, .T. ) ;
#1666=CARTESIAN_POINT ( 'NONE',  ( -58.03335481156723574, 0.8699069336946690933, -4.241846523238430144 ) ) ;
#1689=CARTESIAN_POINT ( 'NONE',  ( -56.54792740578360366, 3.330682475591789871, 0.6830477631804130478 ) ) ;
#1703=EDGE_LOOP ( 'NONE', ( #2562, #14946, #29197, #1747 ) ) ;
#1710=CARTESIAN_POINT ( 'NONE',  ( -60.73542740578358945, -3.725040285533365747, 1.239922660687676093 ) ) ;
#1717=ADVANCED_BREP_SHAPE_REPRESENTATION ( '', ( #25183, #9018 ), #25221 ) ;
#1747=ORIENTED_EDGE ( 'NONE', *, *, #29928, .F. ) ;
#1758=CIRCLE ( 'NONE', #24519, 1.474417381223824153 ) ;
#1774=AXIS2_PLACEMENT_3D ( 'NONE', #16068, #20976, #8758 ) ;
#1791=AXIS2_PLACEMENT_3D ( 'NONE', #10351, #20027, #29670 ) ;
#1802=CIRCLE ( 'NONE', #17505, 4.600000000000000533 ) ;
#1807=CARTESIAN_POINT ( 'NONE',  ( -54.97085481156724285, 2.489203624310592833, -2.804704140674919799 ) ) ;
#1810=CARTESIAN_POINT ( 'NONE',  ( -57.22499999999997300, 2.964020293532818446E-15, 1.549317489258312010E-18 ) ) ;
#1834=CARTESIAN_POINT ( 'NONE',  ( -55.78335481156723574, 0.8699069336946694264, -4.241846523238430144 ) ) ;
#1835=DIRECTION ( 'NONE',  ( 1.000000000000000000, 3.054025858079668409E-16, -2.042474015755241579E-16 ) ) ;
#1839=ORIENTED_EDGE ( 'NONE', *, *, #8570, .T. ) ;
#1859=VECTOR ( 'NONE', #5757, 1000.000000000000000 ) ;
#1863=DIRECTION ( 'NONE',  ( 2.581436205204234006E-16, -0.9796124928211140670, -0.2008964009354148872 ) ) ;
#1864=EDGE_CURVE ( 'NONE', #4537, #9168, #27893, .T. ) ;
#1865=CARTESIAN_POINT ( 'NONE',  ( -56.11042740578360366, -2.936324665650196675, -2.606018187048503076 ) ) ;
#1871=AXIS2_PLACEMENT_3D ( 'NONE', #6443, #8189, #25753 ) ;
#1891=CARTESIAN_POINT ( 'NONE',  ( -55.43749999999997158, 0.8699069336946690933, -4.241846523238429256 ) ) ;
#1896=CARTESIAN_POINT ( 'NONE',  ( -67.99999999999995737, -3.266925685480207642E-16, 2.202315069465528948E-15 ) ) ;
#1911=CARTESIAN_POINT ( 'NONE',  ( -59.29999999999997584, -0.7533615035078030653, 3.673546848079178417 ) ) ;
#1919=CARTESIAN_POINT ( 'NONE',  ( -67.99999999999997158, 0.6177564328764001411, -3.012308415424923780 ) ) ;
#1928=CARTESIAN_POINT ( 'NONE',  ( -56.49999999999997158, -2.489203624310589280, 2.804704140674913582 ) ) ;
#1929=ORIENTED_EDGE ( 'NONE', *, *, #22320, .T. ) ;
#1944=CARTESIAN_POINT ( 'NONE',  ( -58.28335481156723574, -4.108500314926509134, 1.367561758111407677 ) ) ;
#1969=AXIS2_PLACEMENT_3D ( 'NONE', #23194, #25536, #1317 ) ;
#1971=ORIENTED_EDGE ( 'NONE', *, *, #28816, .T. ) ;
#1986=CARTESIAN_POINT ( 'NONE',  ( -60.49999999999995737, 1.963826825011730345E-15, 6.704595576490977020E-16 ) ) ;
#1997=CARTESIAN_POINT ( 'NONE',  ( -58.09585481156723574, -1.184343223768586473, -3.558065644182725418 ) ) ;
#2019=ADVANCED_FACE ( 'NONE', ( #5920 ), #17946, .F. ) ;
#2022=CARTESIAN_POINT ( 'NONE',  ( -55.79792740578360366, 3.330682475591789427, 0.6830477631804118266 ) ) ;
#2024=ORIENTED_EDGE ( 'NONE', *, *, #17179, .F. ) ;
#2043=CARTESIAN_POINT ( 'NONE',  ( -55.81249999999997158, -0.8699069336946620989, 4.241846523238426592 ) ) ;
#2051=EDGE_LOOP ( 'NONE', ( #18958, #15900, #15848, #30933 ) ) ;
#2060=CARTESIAN_POINT ( 'NONE',  ( -55.06684846062113081, -0.2309624077929038066, -3.875409454552791733 ) ) ;
#2080=EDGE_CURVE ( 'NONE', #23979, #15338, #22392, .T. ) ;
#2082=ORIENTED_EDGE ( 'NONE', *, *, #10520, .T. ) ;
#2128=DIRECTION ( 'NONE',  ( 1.000000000000000000, 3.054025858079668409E-16, -2.042474015755241579E-16 ) ) ;
#2149=CARTESIAN_POINT ( 'NONE',  ( -56.29792740578360366, -2.256877952708263635, 2.542931754211924300 ) ) ;
#2153=LINE ( 'NONE', #28915, #3277 ) ;
#2159=FACE_BOUND ( 'NONE', #15755, .T. ) ;
#2161=CARTESIAN_POINT ( 'NONE',  ( -71.49999999999998579, 0.9743475445367603127, -4.751120590182400960 ) ) ;
#2168=CARTESIAN_POINT ( 'NONE',  ( -56.19184846062112371, 0.2309624077929113561, 3.875409454552790844 ) ) ;
#2173=ORIENTED_EDGE ( 'NONE', *, *, #11386, .F. ) ;
#2190=VERTEX_POINT ( 'NONE', #30280 ) ;
#2191=CARTESIAN_POINT ( 'NONE',  ( -55.06249999999997158, -0.8699069336946619879, 4.241846523238426592 ) ) ;
#2220=LINE ( 'NONE', #1919, #29290 ) ;
#2226=EDGE_LOOP ( 'NONE', ( #14269, #5947, #13939, #7004 ) ) ;
#2234=CIRCLE ( 'NONE', #31053, 0.04999999999999989175 ) ;
#2287=ORIENTED_EDGE ( 'NONE', *, *, #26051, .T. ) ;
#2303=ORIENTED_EDGE ( 'NONE', *, *, #10658, .F. ) ;
#2305=CARTESIAN_POINT ( 'NONE',  ( -59.97085481156722864, 1.184343223768590470, 3.558065644182727638 ) ) ;
#2314=( BOUNDED_CURVE ( )  B_SPLINE_CURVE ( 2, ( #10539, #5778, #3418, #7543, #17204, #410, #5472, #5153, #17668 ),
 .UNSPECIFIED., .F., .T. ) 
 B_SPLINE_CURVE_WITH_KNOTS ( ( 3, 2, 2, 2, 3 ),
 ( 0.2500000000000000000, 0.2592592592592592449, 0.2777777777777777901, 0.2962962962962962798, 0.3055555555555555802 ),
 .UNSPECIFIED. ) 
 CURVE ( )  GEOMETRIC_REPRESENTATION_ITEM ( )  RATIONAL_B_SPLINE_CURVE ( ( 0.9330127018922192983, 0.9330127018922194093, 1.000000000000000000, 0.8660254037844387076, 1.000000000000000000, 0.8660254037844387076, 1.000000000000000000, 0.9330127018922191873, 0.9330127018922194093 ) ) 
 REPRESENTATION_ITEM ( '' )  );
#2332=AXIS2_PLACEMENT_3D ( 'NONE', #23085, #1381, #15792 ) ;
#2333=AXIS2_PLACEMENT_3D ( 'NONE', #7561, #19610, #16906 ) ;
#2337=CIRCLE ( 'NONE', #20052, 3.750000000000000444 ) ;
#2358=CARTESIAN_POINT ( 'NONE',  ( -55.87499999999997158, 1.184343223768590692, 3.558065644182724974 ) ) ;
#2369=CYLINDRICAL_SURFACE ( 'NONE', #724, 4.849999999999999645 ) ;
#2372=CARTESIAN_POINT ( 'NONE',  ( -57.72499999999997300, 0.9241234443029108236, -4.506217466977124886 ) ) ;
#2373=LINE ( 'NONE', #12041, #31310 ) ;
#2399=DIRECTION ( 'NONE',  ( 0.000000000000000000, -1.000000000000000000, 0.000000000000000000 ) ) ;
#2416=CARTESIAN_POINT ( 'NONE',  ( -56.90835481156723574, -0.7533615035077978472, 3.673546848079179750 ) ) ;
#2422=AXIS2_PLACEMENT_3D ( 'NONE', #22267, #17199, #5468 ) ;
#2427=ORIENTED_EDGE ( 'NONE', *, *, #21785, .F. ) ;
#2448=CARTESIAN_POINT ( 'NONE',  ( -56.72499999999997300, -0.9241234443029054946, 4.506217466977124886 ) ) ;
#2451=ADVANCED_FACE ( 'NONE', ( #3501 ), #22259, .T. ) ;
#2460=EDGE_CURVE ( 'NONE', #7502, #6162, #1508, .T. ) ;
#2465=CARTESIAN_POINT ( 'NONE',  ( -56.18749999999997868, 0.7533615035078125022, -3.673546848079176641 ) ) ;
#2473=CARTESIAN_POINT ( 'NONE',  ( -58.43749999999997158, 0.7533615035078148336, -3.673546848079175309 ) ) ;
#2477=CARTESIAN_POINT ( 'NONE',  ( -60.53335481156722864, -4.108500314926510022, 1.367561758111408343 ) ) ;
#2495=MECHANICAL_DESIGN_GEOMETRIC_PRESENTATION_REPRESENTATION('',(#4497),#24233);
#2517=DIRECTION ( 'NONE',  ( -1.000000000000000000, -3.054025858079668409E-16, 2.042474015755241579E-16 ) ) ;
#2522=CIRCLE ( 'NONE', #13630, 3.750000000000000444 ) ;
#2527=CARTESIAN_POINT ( 'NONE',  ( -57.62499999999997158, 2.489203624310591056, -2.804704140674917578 ) ) ;
#2536=ORIENTED_EDGE ( 'NONE', *, *, #12223, .F. ) ;
#2545=DIRECTION ( 'NONE',  ( 0.000000000000000000, -0.2008964009354147762, 0.9796124928211140670 ) ) ;
#2560=DIRECTION ( 'NONE',  ( 1.000000000000000000, 3.054025858079668409E-16, -2.042474015755241579E-16 ) ) ;
#2561=CARTESIAN_POINT ( 'NONE',  ( -56.43749999999997158, -4.108500314926507357, 1.367561758111402792 ) ) ;
#2562=ORIENTED_EDGE ( 'NONE', *, *, #22320, .F. ) ;
#2576=DIRECTION ( 'NONE',  ( 0.000000000000000000, -1.000000000000000000, 0.000000000000000000 ) ) ;
#2626=CARTESIAN_POINT ( 'NONE',  ( -54.48542740578361077, 0.7887156198831670739, -3.845940847736174728 ) ) ;
#2630=ORIENTED_EDGE ( 'NONE', *, *, #20852, .F. ) ;
#2667=VERTEX_POINT ( 'NONE', #4436 ) ;
#2673=CARTESIAN_POINT ( 'NONE',  ( -59.99999999999997158, -1.184343223768586251, -3.558065644182723197 ) ) ;
#2677=CARTESIAN_POINT ( 'NONE',  ( -54.50000000000001421, -2.140856255279098619, -2.841089121193913325 ) ) ;
#2701=ORIENTED_EDGE ( 'NONE', *, *, #3718, .T. ) ;
#2720=DIRECTION ( 'NONE',  ( -2.581436205204234499E-16, 0.9796124928211140670, 0.2008964009354147762 ) ) ;
#2722=LINE ( 'NONE', #20309, #17045 ) ;
#2726=EDGE_CURVE ( 'NONE', #9046, #25236, #24063, .T. ) ;
#2749=AXIS2_PLACEMENT_3D ( 'NONE', #7405, #28791, #14531 ) ;
#2752=EDGE_CURVE ( 'NONE', #8907, #6633, #2373, .T. ) ;
#2760=DIRECTION ( 'NONE',  ( -2.614381936396368743E-16, 0.2008964009354147762, -0.9796124928211139560 ) ) ;
#2765=ORIENTED_EDGE ( 'NONE', *, *, #767, .T. ) ;
#2766=CARTESIAN_POINT ( 'NONE',  ( -57.77499999999997016, 2.796048871338436190E-15, 1.138853883557972617E-16 ) ) ;
#2767=CARTESIAN_POINT ( 'NONE',  ( -59.65835481156722864, -3.238593381231841928, -2.874284765127021579 ) ) ;
#2770=ORIENTED_EDGE ( 'NONE', *, *, #10004, .F. ) ;
#2780=CARTESIAN_POINT ( 'NONE',  ( -58.09599364905385244, 0.2309624077928971175, 3.875409454552790844 ) ) ;
#2789=AXIS2_PLACEMENT_3D ( 'NONE', #19017, #28671, #6987 ) ;
#2790=CYLINDRICAL_SURFACE ( 'NONE', #2333, 4.849999999999999645 ) ;
#2801=CIRCLE ( 'NONE', #15935, 1.474464970144730991 ) ;
#2813=CARTESIAN_POINT ( 'NONE',  ( -58.24999999999997158, 3.673546848079180638, 0.7533615035078061739 ) ) ;
#2816=CARTESIAN_POINT ( 'NONE',  ( -55.09599364905386665, 0.2309624077929083863, 3.875409454552789956 ) ) ;
#2848=ORIENTED_EDGE ( 'NONE', *, *, #5186, .F. ) ;
#2850=CARTESIAN_POINT ( 'NONE',  ( -57.59585481156722864, -2.489203624310587060, 2.804704140674918467 ) ) ;
#2858=CARTESIAN_POINT ( 'NONE',  ( -55.54792740578360366, -2.256877952708263191, 2.542931754211924300 ) ) ;
#2864=EDGE_CURVE ( 'NONE', #16804, #25369, #20220, .T. ) ;
#2926=CIRCLE ( 'NONE', #17094, 1.625000000000000444 ) ;
#2935=CARTESIAN_POINT ( 'NONE',  ( -60.54792740578359656, -1.073804522883517576, -3.225979517392334905 ) ) ;
#2948=FACE_OUTER_BOUND ( 'NONE', #7691, .T. ) ;
#2976=ORIENTED_EDGE ( 'NONE', *, *, #26055, .F. ) ;
#2981=DIRECTION ( 'NONE',  ( 0.000000000000000000, -0.2008964009354147484, 0.9796124928211139560 ) ) ;
#2983=VERTEX_POINT ( 'NONE', #11648 ) ;
#2984=CARTESIAN_POINT ( 'NONE',  ( -58.18749999999997158, 3.238593381231845481, 2.874284765127021579 ) ) ;
#3005=EDGE_LOOP ( 'NONE', ( #9050, #29255, #21577, #14217 ) ) ;
#3017=DIRECTION ( 'NONE',  ( 1.000000000000000000, 3.054025858079668409E-16, -2.042474015755241579E-16 ) ) ;
#3020=CARTESIAN_POINT ( 'NONE',  ( -71.44781903063172024, -1.379665415900875831E-15, 2.906523147574707464E-15 ) ) ;
#3042=ADVANCED_FACE ( 'NONE', ( #1648, #18627 ), #18463, .T. ) ;
#3067=DIRECTION ( 'NONE',  ( 0.000000000000000000, -0.2008964009354147484, 0.9796124928211139560 ) ) ;
#3071=ADVANCED_FACE ( 'NONE', ( #18782 ), #13940, .T. ) ;
#3084=CARTESIAN_POINT ( 'NONE',  ( -58.11042740578360366, 3.725040285533370632, -1.239922660687675871 ) ) ;
#3096=VERTEX_POINT ( 'NONE', #9274 ) ;
#3107=CARTESIAN_POINT ( 'NONE',  ( -58.59585481156723574, 3.673546848079181970, 0.7533615035078067290 ) ) ;
#3113=DIRECTION ( 'NONE',  ( -1.000000000000000000, -3.054025858079668409E-16, 2.042474015755241579E-16 ) ) ;
#3123=CARTESIAN_POINT ( 'NONE',  ( -59.29999999999997584, 0.6177564328764025836, -3.012308415424925556 ) ) ;
#3136=CARTESIAN_POINT ( 'NONE',  ( -57.49999999999997158, 3.673546848079180638, 0.7533615035078060629 ) ) ;
#3140=CARTESIAN_POINT ( 'NONE',  ( -54.99999999999997868, -2.489203624310585283, 2.804704140674916690 ) ) ;
#3167=CARTESIAN_POINT ( 'NONE',  ( -54.48542740578361077, 0.7887156198831670739, -3.845940847736174728 ) ) ;
#3210=ORIENTED_EDGE ( 'NONE', *, *, #25069, .F. ) ;
#3224=LINE ( 'NONE', #22548, #7435 ) ;
#3238=CARTESIAN_POINT ( 'NONE',  ( -57.42292740578360366, 2.256877952708269408, -2.542931754211925188 ) ) ;
#3239=CYLINDRICAL_SURFACE ( 'NONE', #2422, 3.750000000000000444 ) ;
#3255=EDGE_CURVE ( 'NONE', #7825, #25236, #31157, .T. ) ;
#3259=ADVANCED_FACE ( 'NONE', ( #6674 ), #9921, .T. ) ;
#3277=VECTOR ( 'NONE', #14339, 1000.000000000000000 ) ;
#3296=CARTESIAN_POINT ( 'NONE',  ( -54.74999999999997868, -1.184343223768585140, -3.558065644182724085 ) ) ;
#3303=CARTESIAN_POINT ( 'NONE',  ( -55.42292740578360366, -3.330682475591782765, -0.6830477631804120486 ) ) ;
#3318=VERTEX_POINT ( 'NONE', #11256 ) ;
#3331=CARTESIAN_POINT ( 'NONE',  ( -59.29999999999998295, -2.410361377416136541, 2.431279660458814718 ) ) ;
#3367=ORIENTED_EDGE ( 'NONE', *, *, #18412, .F. ) ;
#3397=CARTESIAN_POINT ( 'NONE',  ( -55.49999999999997868, -1.184343223768582698, -3.558065644182725418 ) ) ;
#3399=AXIS2_PLACEMENT_3D ( 'NONE', #25028, #25355, #821 ) ;
#3408=ORIENTED_EDGE ( 'NONE', *, *, #16789, .F. ) ;
#3410=CIRCLE ( 'NONE', #10509, 3.598079936076698182 ) ;
#3412=CARTESIAN_POINT ( 'NONE',  ( -56.98542740578360366, -3.725040285533364859, 1.239922660687675204 ) ) ;
#3418=CARTESIAN_POINT ( 'NONE',  ( -55.84585481156723574, -1.184343223768586029, -3.558065644182725862 ) ) ;
#3431=AXIS2_PLACEMENT_3D ( 'NONE', #18805, #23390, #28448 ) ;
#3441=AXIS2_PLACEMENT_3D ( 'NONE', #11042, #25912, #16112 ) ;
#3452=CARTESIAN_POINT ( 'NONE',  ( -54.22085481156724285, 2.489203624310592833, -2.804704140674919799 ) ) ;
#3479=ORIENTED_EDGE ( 'NONE', *, *, #29405, .F. ) ;
#3483=ADVANCED_FACE ( 'NONE', ( #18351 ), #13401, .F. ) ;
#3494=CARTESIAN_POINT ( 'NONE',  ( -56.11042740578360366, -2.936324665650200672, -2.606018187048498191 ) ) ;
#3501=FACE_OUTER_BOUND ( 'NONE', #19557, .T. ) ;
#3539=ORIENTED_EDGE ( 'NONE', *, *, #159, .F. ) ;
#3545=CARTESIAN_POINT ( 'NONE',  ( -59.29999999999997584, 0.7533615035078071731, -3.673546848079177529 ) ) ;
#3551=CARTESIAN_POINT ( 'NONE',  ( -55.47099364905386665, -0.2309624077929001984, -3.875409454552789956 ) ) ;
#3560=B_SPLINE_CURVE_WITH_KNOTS ( 'NONE', 3,
 ( #26754, #15323, #27033, #5518, #15009, #29277, #5344, #10419, #20101, #29736, #2677, #29563, #17104, #5197, #5053, #14707, #8051, #9963 ),
 .UNSPECIFIED., .F., .F.,
 ( 4, 2, 2, 2, 2, 2, 2, 2, 4 ),
 ( 0.000000000000000000, 0.0007653146945936880252, 0.001530629389187376050, 0.002295944083781063967, 0.003061258778374752101, 0.003826573472968439801, 0.004591888167562127067, 0.005357202862155815634, 0.006122517556749502467 ),
 .UNSPECIFIED. ) ;
#3578=CARTESIAN_POINT ( 'NONE',  ( -57.78335481156722864, 3.238593381231847257, 2.874284765127023356 ) ) ;
#3585=CARTESIAN_POINT ( 'NONE',  ( -57.77499999999997016, 2.796048871338436190E-15, 1.138853883557972617E-16 ) ) ;
#3586=CARTESIAN_POINT ( 'NONE',  ( -60.49999999999995737, -0.7328781032566554776, 3.573665542649864246 ) ) ;
#3597=DIRECTION ( 'NONE',  ( -2.614375865348240525E-16, 0.2008964009354147762, -0.9796124928211140670 ) ) ;
#3615=EDGE_CURVE ( 'NONE', #11521, #24734, #17914, .T. ) ;
#3637=CARTESIAN_POINT ( 'NONE',  ( -59.61042740578360366, 3.725040285533370632, -1.239922660687675204 ) ) ;
#3639=CARTESIAN_POINT ( 'NONE',  ( -71.44999999999998863, -0.3062499654112579295, 1.493338310920507839 ) ) ;
#3682=CARTESIAN_POINT ( 'NONE',  ( -60.54999999999995453, 1.948556695721332102E-15, 6.806719277278738347E-16 ) ) ;
#3692=CARTESIAN_POINT ( 'NONE',  ( -59.29999999999994031, 1.532064702718639593, 3.305310576859302518 ) ) ;
#3718=EDGE_CURVE ( 'NONE', #2667, #9046, #25996, .T. ) ;
#3723=VECTOR ( 'NONE', #6519, 1000.000000000000000 ) ;
#3724=AXIS2_PLACEMENT_3D ( 'NONE', #19466, #21704, #14378 ) ;
#3730=EDGE_LOOP ( 'NONE', ( #15344, #21220, #10138, #18219 ) ) ;
#3734=CARTESIAN_POINT ( 'NONE',  ( -55.59585481156724285, 3.673546848079182414, 0.7533615035078059519 ) ) ;
#3756=EDGE_CURVE ( 'NONE', #19802, #25428, #26431, .T. ) ;
#3757=DIRECTION ( 'NONE',  ( 1.000000000000000000, 3.054025858079668409E-16, -2.042474015755241579E-16 ) ) ;
#3759=CARTESIAN_POINT ( 'NONE',  ( -55.04792740578361077, 3.330682475591790315, 0.6830477631804110494 ) ) ;
#3777=SHAPE_REPRESENTATION ( 'Cap', ( #9018 ), #25221 ) ;
#3781=ORIENTED_EDGE ( 'NONE', *, *, #12654, .T. ) ;
#3782=CARTESIAN_POINT ( 'NONE',  ( -56.48542740578359656, 2.936324665650207333, 2.606018187048499080 ) ) ;
#3788=CIRCLE ( 'NONE', #25024, 0.05000000000000009298 ) ;
#3792=AXIS2_PLACEMENT_3D ( 'NONE', #25874, #13813, #27502 ) ;
#3848=CARTESIAN_POINT ( 'NONE',  ( -55.68749999999997158, -4.108500314926507357, 1.367561758111403680 ) ) ;
#3853=CARTESIAN_POINT ( 'NONE',  ( -59.29999999999996163, 0.3064839379836800104, 3.562026904852408471 ) ) ;
#3866=DIRECTION ( 'NONE',  ( 0.000000000000000000, -0.2008964009354147484, 0.9796124928211139560 ) ) ;
#3881=AXIS2_PLACEMENT_3D ( 'NONE', #8290, #17959, #25235 ) ;
#3892=CARTESIAN_POINT ( 'NONE',  ( -58.97085481156723574, -3.673546848079176197, -0.7533615035078063960 ) ) ;
#3895=AXIS2_PLACEMENT_3D ( 'NONE', #1810, #21168, #31105 ) ;
#3902=CARTESIAN_POINT ( 'NONE',  ( -56.53335481156724285, 0.8699069336946694264, -4.241846523238430144 ) ) ;
#3911=DIRECTION ( 'NONE',  ( 1.000000000000000000, 3.054025858079668409E-16, -2.042474015755241579E-16 ) ) ;
#3927=VECTOR ( 'NONE', #13385, 1000.000000000000000 ) ;
#3929=CARTESIAN_POINT ( 'NONE',  ( -58.86042740578361077, 3.725040285533377737, -1.239922660687654554 ) ) ;
#3932=CARTESIAN_POINT ( 'NONE',  ( -56.90835481156724285, -0.7533615035077978472, 3.673546848079179750 ) ) ;
#3941=CARTESIAN_POINT ( 'NONE',  ( -57.72499999999997300, -0.9241234443029058276, 4.506217466977124886 ) ) ;
#3947=CARTESIAN_POINT ( 'NONE',  ( -55.40835481156723574, -0.7533615035078004007, 3.673546848079179306 ) ) ;
#3949=CARTESIAN_POINT ( 'NONE',  ( -58.48542740578359656, -3.725040285533365303, 1.239922660687675648 ) ) ;
#3961=CARTESIAN_POINT ( 'NONE',  ( -55.40835481156723574, -0.7533615035078004007, 3.673546848079179306 ) ) ;
#3964=TOROIDAL_SURFACE ( 'NONE', #25716, 3.250821294908289971, 0.05000000000000000278 ) ;
#3978=DIRECTION ( 'NONE',  ( -1.000000000000000000, -3.054025858079668409E-16, 2.042474015755241579E-16 ) ) ;
#4000=ADVANCED_FACE ( 'NONE', ( #9859 ), #30502, .T. ) ;
#4005=ADVANCED_FACE ( 'NONE', ( #26802 ), #29626, .F. ) ;
#4018=CARTESIAN_POINT ( 'NONE',  ( -60.48535533905928219, 1.968299342331293196E-15, 6.674684237050104391E-16 ) ) ;
#4032=ORIENTED_EDGE ( 'NONE', *, *, #6839, .F. ) ;
#4035=EDGE_CURVE ( 'NONE', #29251, #7998, #6739, .T. ) ;
#4038=CARTESIAN_POINT ( 'NONE',  ( -54.65835481156722864, -0.7533615035078032873, 3.673546848079177973 ) ) ;
#4058=CARTESIAN_POINT ( 'NONE',  ( -59.40835481156722864, 4.108500314926515351, -1.367561758111407455 ) ) ;
#4063=DIRECTION ( 'NONE',  ( 0.000000000000000000, -0.2008964009354152203, 0.9796124928211138450 ) ) ;
#4076=FILL_AREA_STYLE ('',( #18495 ) ) ;
#4081=CARTESIAN_POINT ( 'NONE',  ( -59.29792740578359656, -2.256877952708279178, 2.542931754211911421 ) ) ;
#4103=CARTESIAN_POINT ( 'NONE',  ( -60.61042740578359656, -2.936324665650201560, -2.606018187048497303 ) ) ;
#4118=CARTESIAN_POINT ( 'NONE',  ( -55.09585481156724285, -1.184343223768585807, -3.558065644182726306 ) ) ;
#4154=( BOUNDED_CURVE ( )  B_SPLINE_CURVE ( 2, ( #7300, #14267, #4287, #26616, #16969, #2561, #1928, #16491, #28690 ),
 .UNSPECIFIED., .F., .T. ) 
 B_SPLINE_CURVE_WITH_KNOTS ( ( 3, 2, 2, 2, 3 ),
 ( 0.2500000000000000000, 0.2592592592592592449, 0.2777777777777777901, 0.2962962962962962798, 0.3055555555555555802 ),
 .UNSPECIFIED. ) 
 CURVE ( )  GEOMETRIC_REPRESENTATION_ITEM ( )  RATIONAL_B_SPLINE_CURVE ( ( 0.9330127018922192983, 0.9330127018922194093, 1.000000000000000000, 0.8660254037844387076, 1.000000000000000000, 0.8660254037844387076, 1.000000000000000000, 0.9330127018922191873, 0.9330127018922194093 ) ) 
 REPRESENTATION_ITEM ( '' )  );
#4167=DIRECTION ( 'NONE',  ( 1.000000000000000000, 3.054025858079668409E-16, -2.042474015755241579E-16 ) ) ;
#4185=CARTESIAN_POINT ( 'NONE',  ( -54.90835481156724285, 4.108500314926515351, -1.367561758111408565 ) ) ;
#4207=CARTESIAN_POINT ( 'NONE',  ( -56.40835481156723574, 4.108500314926515351, -1.367561758111408343 ) ) ;
#4229=CARTESIAN_POINT ( 'NONE',  ( -57.36042740578360366, 3.725040285533373741, -1.239922660687670763 ) ) ;
#4233=ADVANCED_FACE ( 'NONE', ( #19023 ), #4447, .F. ) ;
#4245=ORIENTED_EDGE ( 'NONE', *, *, #28550, .T. ) ;
#4251=CARTESIAN_POINT ( 'NONE',  ( -60.17292740578359656, 1.073804522883521351, 3.225979517392337126 ) ) ;
#4279=DIRECTION ( 'NONE',  ( 1.000000000000000000, 3.054025858079668409E-16, -2.042474015755241579E-16 ) ) ;
#4287=CARTESIAN_POINT ( 'NONE',  ( -56.24999999999997158, -1.184343223768582032, -3.558065644182724974 ) ) ;
#4299=CARTESIAN_POINT ( 'NONE',  ( -67.99999999999995737, 0.5554785485864213168, -2.708628542650378890 ) ) ;
#4318=FACE_OUTER_BOUND ( 'NONE', #18719, .T. ) ;
#4321=CARTESIAN_POINT ( 'NONE',  ( -71.49999999999998579, -0.9743475445367636434, 4.751120590182405401 ) ) ;
#4326=VECTOR ( 'NONE', #22014, 1000.000000000000000 ) ;
#4340=AXIS2_PLACEMENT_3D ( 'NONE', #3682, #23011, #6223 ) ;
#4342=CYLINDRICAL_SURFACE ( 'NONE', #30426, 3.750000000000000444 ) ;
#4352=CIRCLE ( 'NONE', #4878, 4.800000000000000711 ) ;
#4364=ORIENTED_EDGE ( 'NONE', *, *, #26969, .T. ) ;
#4367=CARTESIAN_POINT ( 'NONE',  ( -57.15835481156724285, 4.108500314926515351, -1.367561758111408121 ) ) ;
#4392=AXIS2_PLACEMENT_3D ( 'NONE', #15695, #10473, #25342 ) ;
#4394=CYLINDRICAL_SURFACE ( 'NONE', #18549, 3.750000000000000444 ) ;
#4396=CARTESIAN_POINT ( 'NONE',  ( -57.54792740578359656, -1.073804522883506696, -3.225979517392338902 ) ) ;
#4407=ORIENTED_EDGE ( 'NONE', *, *, #13871, .T. ) ;
#4423=CARTESIAN_POINT ( 'NONE',  ( -56.93749999999997158, 0.8699069336946686493, -4.241846523238428368 ) ) ;
#4436=CARTESIAN_POINT ( 'NONE',  ( -54.54999999999998295, -0.9743475445367587584, 4.751120590182401848 ) ) ;
#4438=DIRECTION ( 'NONE',  ( -2.614375865348240525E-16, 0.2008964009354147762, -0.9796124928211140670 ) ) ;
#4447=CYLINDRICAL_SURFACE ( 'NONE', #27230, 3.075000000000000622 ) ;
#4459=DIRECTION ( 'NONE',  ( 0.000000000000000000, 0.2008964009354147762, -0.9796124928211140670 ) ) ;
#4482=EDGE_CURVE ( 'NONE', #9046, #2667, #19172, .T. ) ;
#4497=STYLED_ITEM ( 'NONE', ( #27430 ), #1717 ) ;
#4512=CARTESIAN_POINT ( 'NONE',  ( -54.72085481156724285, 1.184343223768591580, 3.558065644182726750 ) ) ;
#4514=AXIS2_PLACEMENT_3D ( 'NONE', #30626, #23694, #30800 ) ;
#4527=ORIENTED_EDGE ( 'NONE', *, *, #24721, .T. ) ;
#4530=CARTESIAN_POINT ( 'NONE',  ( -55.42292740578360366, -3.330682475591783209, -0.6830477631804113825 ) ) ;
#4537=VERTEX_POINT ( 'NONE', #13408 ) ;
#4556=CARTESIAN_POINT ( 'NONE',  ( -58.48542740578359656, -3.725040285533367523, 1.239922660687669209 ) ) ;
#4557=ADVANCED_FACE ( 'NONE', ( #10747 ), #3964, .T. ) ;
#4577=CARTESIAN_POINT ( 'NONE',  ( -60.36042740578359656, 3.725040285533370632, -1.239922660687674982 ) ) ;
#4587=FACE_OUTER_BOUND ( 'NONE', #3730, .T. ) ;
#4591=CONICAL_SURFACE ( 'NONE', #13658, 2.765000000000001013, 0.03997868712329009228 ) ;
#4606=CARTESIAN_POINT ( 'NONE',  ( -57.28335481156723574, 0.7533615035078095046, -3.673546848079178861 ) ) ;
#4612=CARTESIAN_POINT ( 'NONE',  ( -56.67499999999996874, 3.131991715727200307E-15, -1.107867533772800737E-16 ) ) ;
#4620=DIRECTION ( 'NONE',  ( 0.000000000000000000, 0.2008964009354147484, -0.9796124928211139560 ) ) ;
#4655=ORIENTED_EDGE ( 'NONE', *, *, #28790, .T. ) ;
#4679=CARTESIAN_POINT ( 'NONE',  ( -55.86042740578360366, 3.725040285533370632, -1.239922660687676315 ) ) ;
#4691=DIRECTION ( 'NONE',  ( -1.000000000000000000, -3.054025858079668409E-16, 2.042474015755241579E-16 ) ) ;
#4706=ORIENTED_EDGE ( 'NONE', *, *, #13438, .F. ) ;
#4719=CARTESIAN_POINT ( 'NONE',  ( -54.56249999999997868, 4.108500314926513575, -1.367561758111407899 ) ) ;
#4721=DIRECTION ( 'NONE',  ( -1.000000000000000000, -3.054025858079668409E-16, 2.042474015755241579E-16 ) ) ;
#4727=CARTESIAN_POINT ( 'NONE',  ( -56.99999999999997158, -1.184343223768575371, -3.558065644182727638 ) ) ;
#4730=DIRECTION ( 'NONE',  ( -1.000000000000000000, -3.054025858079668409E-16, 2.042474015755241579E-16 ) ) ;
#4744=EDGE_CURVE ( 'NONE', #333, #20706, #77, .T. ) ;
#4775=DIRECTION ( 'NONE',  ( 1.000000000000000000, 3.054025858079668409E-16, -2.042474015755241579E-16 ) ) ;
#4781=DIRECTION ( 'NONE',  ( -1.000000000000000000, -3.054025858079668409E-16, 2.042474015755241579E-16 ) ) ;
#4811=CARTESIAN_POINT ( 'NONE',  ( -59.29999999999997584, 2.330309927981285032E-15, 4.253626757584724400E-16 ) ) ;
#4822=DIRECTION ( 'NONE',  ( 1.000000000000000000, 3.054025858079668409E-16, -2.042474015755241579E-16 ) ) ;
#4834=CARTESIAN_POINT ( 'NONE',  ( -60.28335481156722864, 0.8699069336946685382, -4.241846523238430144 ) ) ;
#4846=STYLED_ITEM ( 'NONE', ( #932 ), #25183 ) ;
#4869=ORIENTED_EDGE ( 'NONE', *, *, #23870, .T. ) ;
#4873=CIRCLE ( 'NONE', #8419, 0.04999999999999987094 ) ;
#4878=AXIS2_PLACEMENT_3D ( 'NONE', #28110, #4781, #9125 ) ;
#4885=CARTESIAN_POINT ( 'NONE',  ( -58.68749999999997158, -4.108500314926507357, 1.367561758111406789 ) ) ;
#4897=DIRECTION ( 'NONE',  ( 0.7071067811865534569, 0.1420552074174021573, -0.6926906366088618761 ) ) ;
#4906=DIRECTION ( 'NONE',  ( -1.000000000000000000, -3.054025858079668409E-16, 2.042474015755241579E-16 ) ) ;
#4914=DIRECTION ( 'NONE',  ( -1.000000000000000000, -3.054025858079668409E-16, 2.042474015755241579E-16 ) ) ;
#4923=CARTESIAN_POINT ( 'NONE',  ( -71.44999999999998863, -1.380331489585512972E-15, 2.906968604901091669E-15 ) ) ;
#4938=AXIS2_PLACEMENT_3D ( 'NONE', #16567, #16875, #31277 ) ;
#4947=CIRCLE ( 'NONE', #3441, 3.648039984012787507 ) ;
#4950=DIRECTION ( 'NONE',  ( 0.000000000000000000, -0.2008964009354148039, 0.9796124928211140670 ) ) ;
#4958=DIRECTION ( 'NONE',  ( -1.000000000000000000, -3.054025858079668409E-16, 2.042474015755241579E-16 ) ) ;
#4960=ORIENTED_EDGE ( 'NONE', *, *, #1864, .T. ) ;
#4965=VERTEX_POINT ( 'NONE', #7072 ) ;
#4966=ADVANCED_FACE ( 'NONE', ( #5147 ), #29538, .T. ) ;
#4967=ORIENTED_EDGE ( 'NONE', *, *, #6983, .T. ) ;
#4968=CARTESIAN_POINT ( 'NONE',  ( -54.49999999999997868, 3.673546848079182858, 0.7533615035078058408 ) ) ;
#4997=CARTESIAN_POINT ( 'NONE',  ( -55.92292740578360366, 2.256877952708269408, -2.542931754211925632 ) ) ;
#5048=CARTESIAN_POINT ( 'NONE',  ( -60.74999999999996447, -1.184343223768586251, -3.558065644182722753 ) ) ;
#5053=CARTESIAN_POINT ( 'NONE',  ( -54.49999999999994316, -0.7277771693817812748, -3.394129477159102404 ) ) ;
#5055=DIRECTION ( 'NONE',  ( -1.000000000000000000, -3.054027077731387480E-16, 2.042479963029832083E-16 ) ) ;
#5080=EDGE_CURVE ( 'NONE', #6162, #7502, #5803, .T. ) ;
#5081=VERTEX_POINT ( 'NONE', #10359 ) ;
#5084=CARTESIAN_POINT ( 'NONE',  ( -54.86042740578361077, -0.7887156198831597465, 3.845940847736172952 ) ) ;
#5097=DIRECTION ( 'NONE',  ( -2.614375865348241018E-16, 0.2008964009354147762, -0.9796124928211140670 ) ) ;
#5139=VECTOR ( 'NONE', #1153, 1000.000000000000000 ) ;
#5146=ORIENTED_EDGE ( 'NONE', *, *, #28217, .F. ) ;
#5147=FACE_OUTER_BOUND ( 'NONE', #19706, .T. ) ;
#5148=CARTESIAN_POINT ( 'NONE',  ( -60.59585481156722864, -2.489203624310587504, 2.804704140674919355 ) ) ;
#5153=CARTESIAN_POINT ( 'NONE',  ( -56.12486116251334778, -1.737685414808513018, 3.471684241605566879 ) ) ;
#5169=FACE_OUTER_BOUND ( 'NONE', #23417, .T. ) ;
#5186=EDGE_CURVE ( 'NONE', #2667, #7825, #13973, .T. ) ;
#5190=CARTESIAN_POINT ( 'NONE',  ( -67.99999999999995737, -3.266925685480207642E-16, 2.202315069465528948E-15 ) ) ;
#5193=CARTESIAN_POINT ( 'NONE',  ( -59.68749999999997158, 3.238593381231845036, 2.874284765127022023 ) ) ;
#5197=CARTESIAN_POINT ( 'NONE',  ( -54.49999999999997158, -0.9764555328423589753, -3.345672051885957732 ) ) ;
#5210=CARTESIAN_POINT ( 'NONE',  ( -60.54800159808252147, 1.949167012834402697E-15, 6.802637593289325421E-16 ) ) ;
#5228=CARTESIAN_POINT ( 'NONE',  ( -55.23542740578361077, 0.7887156198831668519, -3.845940847736174728 ) ) ;
#5232=CARTESIAN_POINT ( 'NONE',  ( -59.29999999999999716, -3.501719128350677224, -1.006773934787358771 ) ) ;
#5250=DIRECTION ( 'NONE',  ( 2.581436205204234499E-16, -0.9796124928211140670, -0.2008964009354146651 ) ) ;
#5291=CARTESIAN_POINT ( 'NONE',  ( -59.42292740578359656, 1.073804522883521351, 3.225979517392337126 ) ) ;
#5299=DIRECTION ( 'NONE',  ( -1.000000000000000000, -3.054025858079668409E-16, 2.042474015755241579E-16 ) ) ;
#5304=CARTESIAN_POINT ( 'NONE',  ( -59.29999999999997584, 2.330309927981285032E-15, 4.253626757584724400E-16 ) ) ;
#5315=CIRCLE ( 'NONE', #20520, 4.800000000000000711 ) ;
#5317=VERTEX_POINT ( 'NONE', #27233 ) ;
#5318=CARTESIAN_POINT ( 'NONE',  ( -59.29999999999998295, 2.406774162954685714, 2.810364340920085358 ) ) ;
#5322=EDGE_LOOP ( 'NONE', ( #5823, #17092 ) ) ;
#5338=CARTESIAN_POINT ( 'NONE',  ( -58.93749999999996447, 3.238593381231845036, 2.874284765127021579 ) ) ;
#5342=CARTESIAN_POINT ( 'NONE',  ( -55.40400635094609072, 1.737685414808522788, -3.471684241605564658 ) ) ;
#5344=CARTESIAN_POINT ( 'NONE',  ( -54.49999999999996447, -3.201122295486859226, -1.751003668462366880 ) ) ;
#5346=DIRECTION ( 'NONE',  ( -2.614375865348241018E-16, 0.2008964009354147762, -0.9796124928211140670 ) ) ;
#5347=DIRECTION ( 'NONE',  ( 0.000000000000000000, -0.2008964009354148039, 0.9796124928211139560 ) ) ;
#5351=CIRCLE ( 'NONE', #6965, 0.5000000000000013323 ) ;
#5364=CARTESIAN_POINT ( 'NONE',  ( -56.56249999999997158, -0.7533615035078050637, 3.673546848079176197 ) ) ;
#5365=FACE_OUTER_BOUND ( 'NONE', #24098, .T. ) ;
#5370=ORIENTED_EDGE ( 'NONE', *, *, #8979, .T. ) ;
#5378=ORIENTED_EDGE ( 'NONE', *, *, #1864, .F. ) ;
#5422=VERTEX_POINT ( 'NONE', #22662 ) ;
#5427=VERTEX_POINT ( 'NONE', #10609 ) ;
#5438=ORIENTED_EDGE ( 'NONE', *, *, #18029, .F. ) ;
#5440=CIRCLE ( 'NONE', #378, 4.600000000000000533 ) ;
#5467=CARTESIAN_POINT ( 'NONE',  ( -57.23542740578360366, 2.936324665650207333, 2.606018187048499080 ) ) ;
#5468=DIRECTION ( 'NONE',  ( 0.000000000000000000, -0.2008964009354147484, 0.9796124928211139560 ) ) ;
#5472=CARTESIAN_POINT ( 'NONE',  ( -56.09585481156723574, -2.489203624310586616, 2.804704140674918023 ) ) ;
#5479=CARTESIAN_POINT ( 'NONE',  ( -58.31249999999997868, 4.108500314926515351, -1.367561758111400128 ) ) ;
#5480=CARTESIAN_POINT ( 'NONE',  ( -71.44999999999998863, 0.3062499654112550429, -1.493338310920502066 ) ) ;
#5502=CARTESIAN_POINT ( 'NONE',  ( -54.78335481156724285, 3.238593381231848145, 2.874284765127022023 ) ) ;
#5513=CARTESIAN_POINT ( 'NONE',  ( -57.37499999999997158, 1.184343223768590470, 3.558065644182724974 ) ) ;
#5518=CARTESIAN_POINT ( 'NONE',  ( -54.49999999999995737, -3.612379848390220083, -0.8198014738740030394 ) ) ;
#5537=EDGE_LOOP ( 'NONE', ( #10568, #7069, #10179, #17539 ) ) ;
#5566=CARTESIAN_POINT ( 'NONE',  ( -57.22499999999997300, 0.9241234443029110457, -4.506217466977124886 ) ) ;
#5577=CIRCLE ( 'NONE', #23284, 4.849999999999999645 ) ;
#5591=VERTEX_POINT ( 'NONE', #18995 ) ;
#5593=DIRECTION ( 'NONE',  ( -2.581436205204234499E-16, 0.9796124928211140670, 0.2008964009354147762 ) ) ;
#5613=EDGE_CURVE ( 'NONE', #24531, #9415, #13891, .T. ) ;
#5623=CARTESIAN_POINT ( 'NONE',  ( -59.48542740578359656, 2.936324665650206445, 2.606018187048499524 ) ) ;
#5647=ORIENTED_EDGE ( 'NONE', *, *, #6152, .F. ) ;
#5651=ORIENTED_EDGE ( 'NONE', *, *, #19296, .T. ) ;
#5655=CARTESIAN_POINT ( 'NONE',  ( -54.65835481156724995, -0.8699069336946625430, 4.241846523238429256 ) ) ;
#5666=ORIENTED_EDGE ( 'NONE', *, *, #26906, .F. ) ;
#5671=AXIS2_PLACEMENT_3D ( 'NONE', #7054, #26203, #21465 ) ;
#5678=CARTESIAN_POINT ( 'NONE',  ( -55.29792740578360366, -1.073804522883514467, -3.225979517392337126 ) ) ;
#5705=CARTESIAN_POINT ( 'NONE',  ( -59.29999999999999005, -3.566666717976950007, 0.2440603095767059916 ) ) ;
#5710=DIRECTION ( 'NONE',  ( 0.000000000000000000, 0.2008964009354148039, -0.9796124928211140670 ) ) ;
#5722=CARTESIAN_POINT ( 'NONE',  ( -54.49999999999997868, 1.522428981461833253, -3.138047051316147140 ) ) ;
#5745=FACE_OUTER_BOUND ( 'NONE', #14542, .T. ) ;
#5757=DIRECTION ( 'NONE',  ( -1.000000000000000000, -3.054025858079668409E-16, 2.042474015755241579E-16 ) ) ;
#5758=FACE_BOUND ( 'NONE', #23684, .T. ) ;
#5772=CARTESIAN_POINT ( 'NONE',  ( -59.61042740578360366, 3.725040285533370632, -1.239922660687675204 ) ) ;
#5778=CARTESIAN_POINT ( 'NONE',  ( -55.81684846062113792, -0.2309624077929039732, -3.875409454552791733 ) ) ;
#5803=CIRCLE ( 'NONE', #6297, 2.100000000000000089 ) ;
#5823=ORIENTED_EDGE ( 'NONE', *, *, #21949, .T. ) ;
#5824=CARTESIAN_POINT ( 'NONE',  ( -61.18749999999996447, 3.238593381231845036, 2.874284765127022023 ) ) ;
#5832=ORIENTED_EDGE ( 'NONE', *, *, #9863, .F. ) ;
#5846=DIRECTION ( 'NONE',  ( 2.614375865348240525E-16, -0.2008964009354147762, 0.9796124928211140670 ) ) ;
#5859=CARTESIAN_POINT ( 'NONE',  ( -59.17292740578360366, -3.330682475591783653, -0.6830477631804104943 ) ) ;
#5866=( LENGTH_UNIT ( ) NAMED_UNIT ( * ) SI_UNIT ( .MILLI., .METRE. ) );
#5885=CARTESIAN_POINT ( 'NONE',  ( -54.49999999999998579, 3.656246181855014932, -0.5009446076302894735 ) ) ;
#5899=AXIS2_PLACEMENT_3D ( 'NONE', #28531, #31057, #4620 ) ;
#5902=CARTESIAN_POINT ( 'NONE',  ( -54.54999999999998295, 0.9643027244899942119, -4.702139965541348055 ) ) ;
#5904=VERTEX_POINT ( 'NONE', #25129 ) ;
#5920=FACE_OUTER_BOUND ( 'NONE', #20211, .T. ) ;
#5924=CARTESIAN_POINT ( 'NONE',  ( -57.15835481156724285, 4.108500314926515351, -1.367561758111408343 ) ) ;
#5925=AXIS2_PLACEMENT_3D ( 'NONE', #15521, #962, #6318 ) ;
#5933=ORIENTED_EDGE ( 'NONE', *, *, #399, .F. ) ;
#5938=CIRCLE ( 'NONE', #3431, 2.765000000000001013 ) ;
#5941=TOROIDAL_SURFACE ( 'NONE', #19110, 1.524417381223824197, 0.05000000000000000278 ) ;
#5943=CARTESIAN_POINT ( 'NONE',  ( -57.92292740578360366, 1.073804522883521795, 3.225979517392336682 ) ) ;
#5947=ORIENTED_EDGE ( 'NONE', *, *, #3718, .F. ) ;
#5957=CIRCLE ( 'NONE', #6445, 0.04999999999999989175 ) ;
#5971=DIRECTION ( 'NONE',  ( 1.000000000000000000, 3.054025858079668409E-16, -2.042474015755241579E-16 ) ) ;
#5986=CARTESIAN_POINT ( 'NONE',  ( -54.72085481156724285, 1.184343223768591580, 3.558065644182726750 ) ) ;
#5992=VERTEX_POINT ( 'NONE', #12929 ) ;
#6007=LINE ( 'NONE', #27513, #16985 ) ;
#6015=CARTESIAN_POINT ( 'NONE',  ( -67.99999999999997158, -0.3264566515200493790, 1.591870300834312690 ) ) ;
#6030=CARTESIAN_POINT ( 'NONE',  ( -55.74986116251336199, 1.737685414808520790, -3.471684241605567323 ) ) ;
#6031=CARTESIAN_POINT ( 'NONE',  ( -59.48542740578359656, 2.936324665650206445, 2.606018187048499524 ) ) ;
#6042=CARTESIAN_POINT ( 'NONE',  ( -71.44999999999998863, -1.380331489585512972E-15, 2.906968604901091669E-15 ) ) ;
#6047=CARTESIAN_POINT ( 'NONE',  ( -60.49999999999995737, 1.963826825011730345E-15, 6.704595576490977020E-16 ) ) ;
#6063=VERTEX_POINT ( 'NONE', #6449 ) ;
#6089=CARTESIAN_POINT ( 'NONE',  ( -59.92928932188130631, -0.9643027244899888828, 4.702139965541348055 ) ) ;
#6109=CARTESIAN_POINT ( 'NONE',  ( -58.43749999999997158, 0.7533615035078148336, -3.673546848079175309 ) ) ;
#6112=EDGE_CURVE ( 'NONE', #13558, #28004, #5938, .T. ) ;
#6120=CARTESIAN_POINT ( 'NONE',  ( -58.78335481156722864, 0.7533615035077975142, -3.673546848079180638 ) ) ;
#6131=CARTESIAN_POINT ( 'NONE',  ( -56.22085481156723574, 1.184343223768591358, 3.558065644182726750 ) ) ;
#6133=CARTESIAN_POINT ( 'NONE',  ( -69.22071067811863543, -6.995007661688606141E-16, 2.451642053546763754E-15 ) ) ;
#6150=AXIS2_PLACEMENT_3D ( 'NONE', #11215, #20888, #30517 ) ;
#6152=EDGE_CURVE ( 'NONE', #26216, #9570, #2926, .T. ) ;
#6162=VERTEX_POINT ( 'NONE', #17347 ) ;
#6177=CARTESIAN_POINT ( 'NONE',  ( -56.79792740578360366, -1.073804522883517132, -3.225979517392335794 ) ) ;
#6178=DIRECTION ( 'NONE',  ( 0.000000000000000000, 0.2008964009354147484, -0.9796124928211139560 ) ) ;
#6192=CARTESIAN_POINT ( 'NONE',  ( -54.49999999999997158, 3.695864355900486231, -0.2535994654912652191 ) ) ;
#6223=DIRECTION ( 'NONE',  ( -2.614375865348240525E-16, 0.2008964009354147484, -0.9796124928211139560 ) ) ;
#6239=PRODUCT_DEFINITION ( 'UNKNOWN', '', #17706, #17737 ) ;
#6244=ORIENTED_EDGE ( 'NONE', *, *, #24488, .F. ) ;
#6255=EDGE_CURVE ( 'NONE', #11263, #16493, #25161, .T. ) ;
#6270=ORIENTED_EDGE ( 'NONE', *, *, #11386, .T. ) ;
#6276=CARTESIAN_POINT ( 'NONE',  ( -58.59585481156723574, 3.673546848079181970, 0.7533615035078067290 ) ) ;
#6277=DIRECTION ( 'NONE',  ( -1.000000000000000000, -3.054025858079668409E-16, 2.042474015755241579E-16 ) ) ;
#6288=CARTESIAN_POINT ( 'NONE',  ( -60.24999999999997868, 0.6177564328764024726, -3.012308415424925556 ) ) ;
#6297=AXIS2_PLACEMENT_3D ( 'NONE', #17662, #551, #13197 ) ;
#6298=CARTESIAN_POINT ( 'NONE',  ( -58.73542740578359656, 2.936324665650196675, 2.606018187048510626 ) ) ;
#6300=CARTESIAN_POINT ( 'NONE',  ( -56.78335481156722864, -4.108500314926509134, 1.367561758111407455 ) ) ;
#6318=DIRECTION ( 'NONE',  ( 0.000000000000000000, 0.2008964009354162750, -0.9796124928211136229 ) ) ;
#6320=CARTESIAN_POINT ( 'NONE',  ( -58.17292740578360366, 2.256877952708268964, -2.542931754211925188 ) ) ;
#6325=AXIS2_PLACEMENT_3D ( 'NONE', #6402, #20973, #3866 ) ;
#6334=DIRECTION ( 'NONE',  ( -1.000000000000000000, -3.054025858079668409E-16, 2.042474015755241579E-16 ) ) ;
#6338=DIRECTION ( 'NONE',  ( 0.000000000000000000, 0.2008964009354147762, -0.9796124928211139560 ) ) ;
#6340=CARTESIAN_POINT ( 'NONE',  ( -54.49999999999997868, 3.673546848079182858, 0.7533615035078058408 ) ) ;
#6363=CYLINDRICAL_SURFACE ( 'NONE', #26727, 3.750000000000000444 ) ;
#6364=ORIENTED_EDGE ( 'NONE', *, *, #6152, .T. ) ;
#6377=CIRCLE ( 'NONE', #6907, 4.279289321881344144 ) ;
#6378=( BOUNDED_CURVE ( )  B_SPLINE_CURVE ( 2, ( #25064, #3551, #3397, #15876, #13188, #3848, #18426, #11131, #29827 ),
 .UNSPECIFIED., .F., .T. ) 
 B_SPLINE_CURVE_WITH_KNOTS ( ( 3, 2, 2, 2, 3 ),
 ( 0.1388888888888888951, 0.1481481481481481399, 0.1666666666666666574, 0.1851851851851851749, 0.1944444444444444475 ),
 .UNSPECIFIED. ) 
 CURVE ( )  GEOMETRIC_REPRESENTATION_ITEM ( )  RATIONAL_B_SPLINE_CURVE ( ( 0.9330127018922192983, 0.9330127018922194093, 1.000000000000000000, 0.8660254037844387076, 1.000000000000000000, 0.8660254037844387076, 1.000000000000000000, 0.9330127018922191873, 0.9330127018922192983 ) ) 
 REPRESENTATION_ITEM ( '' )  );
#6396=CARTESIAN_POINT ( 'NONE',  ( -60.86042740578358945, -0.7887156198831608567, 3.845940847736174728 ) ) ;
#6402=CARTESIAN_POINT ( 'NONE',  ( -59.29999999999997584, 2.330309927981285032E-15, 4.253626757584724400E-16 ) ) ;
#6410=CIRCLE ( 'NONE', #10967, 4.835355339059328017 ) ;
#6434=FACE_OUTER_BOUND ( 'NONE', #16540, .T. ) ;
#6442=CARTESIAN_POINT ( 'NONE',  ( -56.84585481156722864, -2.489203624310586616, 2.804704140674918467 ) ) ;
#6443=CARTESIAN_POINT ( 'NONE',  ( -69.18535533905931345, -6.887031541980249260E-16, 2.444420817412074983E-15 ) ) ;
#6445=AXIS2_PLACEMENT_3D ( 'NONE', #16265, #18808, #26234 ) ;
#6449=CARTESIAN_POINT ( 'NONE',  ( -60.49999999999995737, 0.8596938233273154761, -4.192045280110956895 ) ) ;
#6465=DIRECTION ( 'NONE',  ( 0.000000000000000000, 0.2008964009354147207, -0.9796124928211139560 ) ) ;
#6468=CARTESIAN_POINT ( 'NONE',  ( -58.11042740578360366, 3.725040285533373741, -1.239922660687669209 ) ) ;
#6484=CARTESIAN_POINT ( 'NONE',  ( -59.29999999999997584, 0.7533615035078071731, -3.673546848079177529 ) ) ;
#6486=CARTESIAN_POINT ( 'NONE',  ( -57.61042740578359656, -2.936324665650201116, -2.606018187048497747 ) ) ;
#6508=CIRCLE ( 'NONE', #1969, 3.300781342844381072 ) ;
#6519=DIRECTION ( 'NONE',  ( 0.7071067811865484609, 0.1420552074174031565, -0.6926906366088668721 ) ) ;
#6561=DIRECTION ( 'NONE',  ( -2.581436205204234499E-16, 0.9796124928211140670, 0.2008964009354147762 ) ) ;
#6588=CARTESIAN_POINT ( 'NONE',  ( -56.12499999999997868, 2.489203624310595497, -2.804704140674914470 ) ) ;
#6597=CARTESIAN_POINT ( 'NONE',  ( -56.78335481156722864, -4.108500314926510022, 1.367561758111407455 ) ) ;
#6619=CARTESIAN_POINT ( 'NONE',  ( -56.92292740578359656, -3.330682475591782765, -0.6830477631804132699 ) ) ;
#6633=VERTEX_POINT ( 'NONE', #15566 ) ;
#6640=CARTESIAN_POINT ( 'NONE',  ( -56.56249999999997158, -0.8699069336946623210, 4.241846523238426592 ) ) ;
#6653=CARTESIAN_POINT ( 'NONE',  ( -69.22071067811863543, -6.995007661688606141E-16, 2.451642053546763754E-15 ) ) ;
#6660=ORIENTED_EDGE ( 'NONE', *, *, #13138, .T. ) ;
#6664=CARTESIAN_POINT ( 'NONE',  ( -57.77499999999997016, 0.9743475445367644205, -4.751120590182402736 ) ) ;
#6674=FACE_OUTER_BOUND ( 'NONE', #22562, .T. ) ;
#6675=ORIENTED_EDGE ( 'NONE', *, *, #25846, .T. ) ;
#6690=DIRECTION ( 'NONE',  ( -1.000000000000000000, -3.054025858079668409E-16, 2.042474015755241579E-16 ) ) ;
#6691=CARTESIAN_POINT ( 'NONE',  ( -57.81249999999997158, -3.238593381231830381, -2.874284765127031793 ) ) ;
#6707=ORIENTED_EDGE ( 'NONE', *, *, #10930, .F. ) ;
#6716=( BOUNDED_CURVE ( )  B_SPLINE_CURVE ( 2, ( #29691, #2780, #12432, #24630, #27320, #5479, #7835, #17350, #563 ),
 .UNSPECIFIED., .F., .T. ) 
 B_SPLINE_CURVE_WITH_KNOTS ( ( 3, 2, 2, 2, 3 ),
 ( 0.5277777777777777901, 0.5370370370370370905, 0.5555555555555555802, 0.5740740740740740700, 0.5833333333333333703 ),
 .UNSPECIFIED. ) 
 CURVE ( )  GEOMETRIC_REPRESENTATION_ITEM ( )  RATIONAL_B_SPLINE_CURVE ( ( 0.9330127018922194093, 0.9330127018922194093, 1.000000000000000000, 0.8660254037844387076, 1.000000000000000000, 0.8660254037844387076, 1.000000000000000000, 0.9330127018922189652, 0.9330127018922194093 ) ) 
 REPRESENTATION_ITEM ( '' )  );
#6724=CARTESIAN_POINT ( 'NONE',  ( -57.22499999999997300, -0.9241234443029057166, 4.506217466977124886 ) ) ;
#6726=ORIENTED_EDGE ( 'NONE', *, *, #17179, .T. ) ;
#6739=CIRCLE ( 'NONE', #27980, 4.849999999999999645 ) ;
#6742=VERTEX_POINT ( 'NONE', #6288 ) ;
#6744=CARTESIAN_POINT ( 'NONE',  ( -56.09585481156723574, -2.489203624310586616, 2.804704140674918023 ) ) ;
#6747=ORIENTED_EDGE ( 'NONE', *, *, #21625, .F. ) ;
#6753=EDGE_LOOP ( 'NONE', ( #28633, #16768, #20848, #28641 ) ) ;
#6767=CARTESIAN_POINT ( 'NONE',  ( -56.34585481156723574, 3.673546848079182858, 0.7533615035078061739 ) ) ;
#6768=CARTESIAN_POINT ( 'NONE',  ( -56.36042740578360366, -0.7887156198831688503, 3.845940847736172064 ) ) ;
#6792=CARTESIAN_POINT ( 'NONE',  ( -55.93749999999997868, 3.238593381231845481, 2.874284765127021579 ) ) ;
#6824=EDGE_CURVE ( 'NONE', #9750, #24313, #10114, .T. ) ;
#6839=EDGE_CURVE ( 'NONE', #29380, #7998, #7084, .T. ) ;
#6845=AXIS2_PLACEMENT_3D ( 'NONE', #10027, #5250, #11919 ) ;
#6846=DIRECTION ( 'NONE',  ( 0.000000000000000000, -0.2008964009354147484, 0.9796124928211138450 ) ) ;
#6858=ORIENTED_EDGE ( 'NONE', *, *, #12693, .F. ) ;
#6861=CARTESIAN_POINT ( 'NONE',  ( -58.93749999999997158, 3.238593381231834378, 2.874284765127034014 ) ) ;
#6900=CARTESIAN_POINT ( 'NONE',  ( -57.65835481156722864, -0.7533615035078039535, 3.673546848079178861 ) ) ;
#6901=AXIS2_PLACEMENT_3D ( 'NONE', #26975, #7670, #2760 ) ;
#6906=ORIENTED_EDGE ( 'NONE', *, *, #24354, .F. ) ;
#6907=AXIS2_PLACEMENT_3D ( 'NONE', #6047, #20622, #6338 ) ;
#6912=( BOUNDED_CURVE ( )  B_SPLINE_CURVE ( 2, ( #11866, #16642, #4727, #21394, #23436, #9342, #21547, #26281, #1573 ),
 .UNSPECIFIED., .F., .T. ) 
 B_SPLINE_CURVE_WITH_KNOTS ( ( 3, 2, 2, 2, 3 ),
 ( 0.3611111111111111605, 0.3703703703703703498, 0.3888888888888888951, 0.4074074074074073848, 0.4166666666666666852 ),
 .UNSPECIFIED. ) 
 CURVE ( )  GEOMETRIC_REPRESENTATION_ITEM ( )  RATIONAL_B_SPLINE_CURVE ( ( 0.9330127018922194093, 0.9330127018922197424, 1.000000000000000000, 0.8660254037844387076, 1.000000000000000000, 0.8660254037844387076, 1.000000000000000000, 0.9330127018922191873, 0.9330127018922194093 ) ) 
 REPRESENTATION_ITEM ( '' )  );
#6914=CARTESIAN_POINT ( 'NONE',  ( -60.40835481156722153, -3.238593381231841928, -2.874284765127021579 ) ) ;
#6937=AXIS2_PLACEMENT_3D ( 'NONE', #20346, #1612, #6846 ) ;
#6942=CARTESIAN_POINT ( 'NONE',  ( -55.86042740578360366, 3.725040285533371520, -1.239922660687672540 ) ) ;
#6965=AXIS2_PLACEMENT_3D ( 'NONE', #5566, #12222, #189 ) ;
#6967=CARTESIAN_POINT ( 'NONE',  ( -60.92292740578359656, 1.073804522883521351, 3.225979517392337570 ) ) ;
#6969=CARTESIAN_POINT ( 'NONE',  ( -54.65835481156722864, -0.7533615035078032873, 3.673546848079177973 ) ) ;
#6983=EDGE_CURVE ( 'NONE', #11953, #13554, #20219, .T. ) ;
#6987=DIRECTION ( 'NONE',  ( 0.000000000000000000, 0.2008964009354147762, -0.9796124928211139560 ) ) ;
#6995=DIRECTION ( 'NONE',  ( 0.000000000000000000, 0.2008964009354147484, -0.9796124928211139560 ) ) ;
#7002=AXIS2_PLACEMENT_3D ( 'NONE', #5190, #27027, #2981 ) ;
#7003=EDGE_CURVE ( 'NONE', #11632, #21265, #6716, .T. ) ;
#7004=ORIENTED_EDGE ( 'NONE', *, *, #15291, .F. ) ;
#7022=DIRECTION ( 'NONE',  ( -2.614375865348240525E-16, 0.2008964009354147762, -0.9796124928211140670 ) ) ;
#7029=CARTESIAN_POINT ( 'NONE',  ( -57.22499999999997300, 2.964020293532818446E-15, 1.549317489258312010E-18 ) ) ;
#7037=EDGE_LOOP ( 'NONE', ( #21995, #18003, #29146, #13715 ) ) ;
#7039=CARTESIAN_POINT ( 'NONE',  ( -71.49999999999998579, -1.395601618875910821E-15, 2.917180974979867506E-15 ) ) ;
#7054=CARTESIAN_POINT ( 'NONE',  ( -59.29999999999997584, 2.330309927981285032E-15, 4.253626757584724400E-16 ) ) ;
#7069=ORIENTED_EDGE ( 'NONE', *, *, #10658, .T. ) ;
#7072=CARTESIAN_POINT ( 'NONE',  ( -60.49999999999995737, -0.8596938233273121455, 4.192045280110958672 ) ) ;
#7073=CARTESIAN_POINT ( 'NONE',  ( -59.59585481156723574, -1.184343223768586695, -3.558065644182724974 ) ) ;
#7084=LINE ( 'NONE', #2161, #24266 ) ;
#7086=DIRECTION ( 'NONE',  ( -1.000000000000000000, -3.054025858079668409E-16, 2.042474015755241579E-16 ) ) ;
#7120=CARTESIAN_POINT ( 'NONE',  ( -60.29792740578359656, 3.330682475591789427, 0.6830477631804114935 ) ) ;
#7150=VERTEX_POINT ( 'NONE', #27937 ) ;
#7179=CARTESIAN_POINT ( 'NONE',  ( -67.99999999999997158, -3.266925685480240183E-16, 2.202315069465531314E-15 ) ) ;
#7207=DIRECTION ( 'NONE',  ( -1.000000000000000000, -3.054025858079668409E-16, 2.042474015755241579E-16 ) ) ;
#7221=CARTESIAN_POINT ( 'NONE',  ( -59.53335481156722864, 0.8699069336946687603, -4.241846523238430144 ) ) ;
#7260=CARTESIAN_POINT ( 'NONE',  ( -56.68749999999997158, 3.238593381231846369, 2.874284765127021579 ) ) ;
#7295=CARTESIAN_POINT ( 'NONE',  ( -57.40835481156722864, -3.238593381231842816, -2.874284765127022023 ) ) ;
#7300=CARTESIAN_POINT ( 'NONE',  ( -56.18749999999997868, 0.7533615035078125022, -3.673546848079176641 ) ) ;
#7355=DIRECTION ( 'NONE',  ( 0.9992009587217894895, -0.008029435056736644594, 0.03915318968010782219 ) ) ;
#7360=CARTESIAN_POINT ( 'NONE',  ( -67.99999999999997158, -3.266925685480240183E-16, 2.202315069465531314E-15 ) ) ;
#7371=CARTESIAN_POINT ( 'NONE',  ( -56.42292740578360366, 1.073804522883522239, 3.225979517392336238 ) ) ;
#7375=CIRCLE ( 'NONE', #22053, 4.800000000000000711 ) ;
#7382=ORIENTED_EDGE ( 'NONE', *, *, #9759, .F. ) ;
#7387=CARTESIAN_POINT ( 'NONE',  ( -69.22071067811863543, 0.4218824419643703583, -2.057186234924337054 ) ) ;
#7403=DIRECTION ( 'NONE',  ( -1.000000000000000000, -3.054025858079668409E-16, 2.042474015755241579E-16 ) ) ;
#7405=CARTESIAN_POINT ( 'NONE',  ( -71.44999999999998863, -1.380331489585512972E-15, 2.906968604901091669E-15 ) ) ;
#7426=CARTESIAN_POINT ( 'NONE',  ( -60.24999999999996447, -2.489203624310586171, 2.804704140674917578 ) ) ;
#7432=CARTESIAN_POINT ( 'NONE',  ( -54.93749999999997158, -4.108500314926507357, 1.367561758111405901 ) ) ;
#7435=VECTOR ( 'NONE', #10518, 1000.000000000000000 ) ;
#7437=EDGE_LOOP ( 'NONE', ( #3781, #27068, #1601, #28594 ) ) ;
#7463=CARTESIAN_POINT ( 'NONE',  ( -54.36042740578361077, 3.725040285533371076, -1.239922660687676537 ) ) ;
#7485=VECTOR ( 'NONE', #9844, 999.9999999999998863 ) ;
#7492=ORIENTED_EDGE ( 'NONE', *, *, #4482, .F. ) ;
#7499=EDGE_LOOP ( 'NONE', ( #27625, #26782, #20400, #2770 ) ) ;
#7502=VERTEX_POINT ( 'NONE', #24588 ) ;
#7524=APPLICATION_CONTEXT ( 'automotive_design' ) ;
#7530=FACE_OUTER_BOUND ( 'NONE', #7570, .T. ) ;
#7538=CARTESIAN_POINT ( 'NONE',  ( -54.36042740578361077, 3.725040285533371076, -1.239922660687676537 ) ) ;
#7543=CARTESIAN_POINT ( 'NONE',  ( -55.90835481156722864, -3.238593381231841928, -2.874284765127022467 ) ) ;
#7549=DIRECTION ( 'NONE',  ( 0.9992009587217894895, 0.008029435056737250012, -0.03915318968010823159 ) ) ;
#7561=CARTESIAN_POINT ( 'NONE',  ( -71.49999999999998579, -1.395601618875910821E-15, 2.917180974979867506E-15 ) ) ;
#7570=EDGE_LOOP ( 'NONE', ( #30227, #5651 ) ) ;
#7584=CARTESIAN_POINT ( 'NONE',  ( -58.12499999999997158, 1.184343223768590248, 3.558065644182725418 ) ) ;
#7597=ADVANCED_FACE ( 'NONE', ( #218 ), #4591, .F. ) ;
#7600=VECTOR ( 'NONE', #7549, 999.9999999999998863 ) ;
#7621=CARTESIAN_POINT ( 'NONE',  ( -59.29999999999996163, -3.145551863026063266, -1.948307423342382938 ) ) ;
#7635=CARTESIAN_POINT ( 'NONE',  ( -69.19999999999998863, -6.931756715175872842E-16, 2.447411951356162049E-15 ) ) ;
#7670=DIRECTION ( 'NONE',  ( -1.000000000000000000, -3.054027077731387480E-16, 2.042479963029832083E-16 ) ) ;
#7672=CARTESIAN_POINT ( 'NONE',  ( -56.67499999999996874, 0.9643027244899941008, -4.702139965541347166 ) ) ;
#7679=CARTESIAN_POINT ( 'NONE',  ( -60.11042740578358945, -0.7887156198831607457, 3.845940847736174728 ) ) ;
#7691=EDGE_LOOP ( 'NONE', ( #4869, #17930 ) ) ;
#7715=DIRECTION ( 'NONE',  ( 0.000000000000000000, 0.2008964009354147484, -0.9796124928211139560 ) ) ;
#7722=CARTESIAN_POINT ( 'NONE',  ( -57.99999999999997158, -2.489203624310585727, 2.804704140674917134 ) ) ;
#7724=EDGE_CURVE ( 'NONE', #9570, #26216, #24308, .T. ) ;
#7727=( BOUNDED_CURVE ( )  B_SPLINE_CURVE ( 2, ( #21390, #14233, #11861, #29564, #27208 ),
 .UNSPECIFIED., .F., .T. ) 
 B_SPLINE_CURVE_WITH_KNOTS ( ( 3, 2, 3 ),
 ( 0.6944444444444445308, 0.7037037037037037202, 0.7112308204265433975 ),
 .UNSPECIFIED. ) 
 CURVE ( )  GEOMETRIC_REPRESENTATION_ITEM ( )  RATIONAL_B_SPLINE_CURVE ( ( 0.9330127018922194093, 0.9330127018922197424, 1.000000000000000000, 0.9455441091250682550, 0.9353569697112142922 ) ) 
 REPRESENTATION_ITEM ( '' )  );
#7805=DIRECTION ( 'NONE',  ( 1.000000000000000000, 3.054025858079668409E-16, -2.042474015755241579E-16 ) ) ;
#7822=CARTESIAN_POINT ( 'NONE',  ( -60.73542740578358945, -3.725040285533365747, 1.239922660687676093 ) ) ;
#7825=VERTEX_POINT ( 'NONE', #23905 ) ;
#7835=CARTESIAN_POINT ( 'NONE',  ( -58.37499999999997158, 2.489203624310597274, -2.804704140674911361 ) ) ;
#7846=TOROIDAL_SURFACE ( 'NONE', #11403, 4.600000000000000533, 0.5000000000000013323 ) ;
#7875=CARTESIAN_POINT ( 'NONE',  ( -57.24999999999996447, -2.489203624310585283, 2.804704140674917134 ) ) ;
#7889=EDGE_CURVE ( 'NONE', #7150, #9227, #7727, .T. ) ;
#7932=TOROIDAL_SURFACE ( 'NONE', #16025, 4.800000000000000711, 0.05000000000000000278 ) ;
#7944=AXIS2_PLACEMENT_3D ( 'NONE', #20531, #11163, #18462 ) ;
#7951=CARTESIAN_POINT ( 'NONE',  ( -67.99999999999997158, -3.266925685480267300E-16, 2.202315069465532498E-15 ) ) ;
#7968=( NAMED_UNIT ( * ) SI_UNIT ( $, .STERADIAN. ) SOLID_ANGLE_UNIT ( ) );
#7983=AXIS2_PLACEMENT_3D ( 'NONE', #30288, #18588, #22871 ) ;
#7988=CARTESIAN_POINT ( 'NONE',  ( -57.09585481156723574, 3.673546848079182414, 0.7533615035078063960 ) ) ;
#7998=VERTEX_POINT ( 'NONE', #30035 ) ;
#8000=CARTESIAN_POINT ( 'NONE',  ( -59.86042740578359656, -2.936324665650201116, -2.606018187048497303 ) ) ;
#8034=CARTESIAN_POINT ( 'NONE',  ( -55.34585481156723574, -2.489203624310586616, 2.804704140674918023 ) ) ;
#8046=CARTESIAN_POINT ( 'NONE',  ( -59.49999999999997158, -2.489203624310586171, 2.804704140674917578 ) ) ;
#8051=CARTESIAN_POINT ( 'NONE',  ( -54.49999999999998579, 0.03583423507999000668, -3.425661966777131973 ) ) ;
#8079=AXIS2_PLACEMENT_3D ( 'NONE', #9767, #18810, #19285 ) ;
#8087=DIRECTION ( 'NONE',  ( -1.000000000000000000, -3.054025858079668409E-16, 2.042474015755241579E-16 ) ) ;
#8116=CARTESIAN_POINT ( 'NONE',  ( -55.40835481156723574, -0.7533615035078004007, 3.673546848079179306 ) ) ;
#8150=CARTESIAN_POINT ( 'NONE',  ( -58.17292740578360366, 2.256877952708268964, -2.542931754211925188 ) ) ;
#8176=CARTESIAN_POINT ( 'NONE',  ( -58.40835481156724285, -0.7533615035077920741, 3.673546848079180638 ) ) ;
#8186=ORIENTED_EDGE ( 'NONE', *, *, #26897, .T. ) ;
#8189=DIRECTION ( 'NONE',  ( 1.000000000000000000, 3.054025858079668409E-16, -2.042474015755241579E-16 ) ) ;
#8197=CARTESIAN_POINT ( 'NONE',  ( -56.72499999999997300, -0.9643027244899884387, 4.702139965541347166 ) ) ;
#8200=AXIS2_PLACEMENT_3D ( 'NONE', #17064, #7086, #19751 ) ;
#8201=DIRECTION ( 'NONE',  ( -1.000000000000000000, -3.054025858079668409E-16, 2.042474015755241579E-16 ) ) ;
#8230=CARTESIAN_POINT ( 'NONE',  ( -58.73542740578359656, 2.936324665650206889, 2.606018187048499080 ) ) ;
#8232=FACE_OUTER_BOUND ( 'NONE', #14769, .T. ) ;
#8264=ORIENTED_EDGE ( 'NONE', *, *, #30713, .F. ) ;
#8267=ORIENTED_EDGE ( 'NONE', *, *, #10520, .F. ) ;
#8277=CARTESIAN_POINT ( 'NONE',  ( -57.31249999999996447, -0.7533615035078060629, 3.673546848079176197 ) ) ;
#8290=CARTESIAN_POINT ( 'NONE',  ( -57.72499999999997300, 2.811319000628834039E-15, 1.036730182770210180E-16 ) ) ;
#8296=ORIENTED_EDGE ( 'NONE', *, *, #25943, .F. ) ;
#8298=CARTESIAN_POINT ( 'NONE',  ( -57.48542740578361077, 0.7887156198831664078, -3.845940847736174284 ) ) ;
#8312=CIRCLE ( 'NONE', #24014, 0.04999999999999988481 ) ;
#8314=CARTESIAN_POINT ( 'NONE',  ( -57.65835481156722864, -0.7533615035078039535, 3.673546848079178861 ) ) ;
#8327=AXIS2_PLACEMENT_3D ( 'NONE', #18128, #20803, #30433 ) ;
#8333=ORIENTED_EDGE ( 'NONE', *, *, #6824, .T. ) ;
#8336=FACE_OUTER_BOUND ( 'NONE', #26707, .T. ) ;
#8375=VECTOR ( 'NONE', #11719, 1000.000000000000000 ) ;
#8380=CARTESIAN_POINT ( 'NONE',  ( -58.61042740578358945, -0.7887156198831605236, 3.845940847736174284 ) ) ;
#8387=ORIENTED_EDGE ( 'NONE', *, *, #9373, .F. ) ;
#8389=AXIS2_PLACEMENT_3D ( 'NONE', #1986, #16084, #11307 ) ;
#8415=ORIENTED_EDGE ( 'NONE', *, *, #27305, .T. ) ;
#8419=AXIS2_PLACEMENT_3D ( 'NONE', #29003, #26469, #17143 ) ;
#8450=CARTESIAN_POINT ( 'NONE',  ( -60.49999999999995737, 0.7328781032566589193, -3.573665542649862914 ) ) ;
#8452=VECTOR ( 'NONE', #4279, 1000.000000000000000 ) ;
#8462=DIRECTION ( 'NONE',  ( -1.000000000000000000, -3.054025858079668409E-16, 2.042474015755241579E-16 ) ) ;
#8485=CARTESIAN_POINT ( 'NONE',  ( -71.49999999999998579, -1.395601618875910821E-15, 2.917180974979867506E-15 ) ) ;
#8489=DIRECTION ( 'NONE',  ( 0.000000000000000000, -0.2008964009354147762, 0.9796124928211140670 ) ) ;
#8490=CARTESIAN_POINT ( 'NONE',  ( -59.03335481156722864, -4.108500314926510022, 1.367561758111408121 ) ) ;
#8499=CARTESIAN_POINT ( 'NONE',  ( -57.28335481156723574, 0.8699069336946692044, -4.241846523238430144 ) ) ;
#8504=CARTESIAN_POINT ( 'NONE',  ( -71.49999999999998579, -1.395601618875910821E-15, 2.917180974979867506E-15 ) ) ;
#8505=EDGE_CURVE ( 'NONE', #1074, #8907, #10187, .T. ) ;
#8522=CARTESIAN_POINT ( 'NONE',  ( -54.67292740578360366, -3.330682475591782765, -0.6830477631804114935 ) ) ;
#8541=CARTESIAN_POINT ( 'NONE',  ( -56.04792740578360366, -1.073804522883516688, -3.225979517392335794 ) ) ;
#8570=EDGE_CURVE ( 'NONE', #21265, #9091, #16425, .T. ) ;
#8574=LINE ( 'NONE', #9084, #12757 ) ;
#8584=ORIENTED_EDGE ( 'NONE', *, *, #1261, .F. ) ;
#8607=ADVANCED_FACE ( 'NONE', ( #21635 ), #11790, .F. ) ;
#8612=ADVANCED_FACE ( 'NONE', ( #14163 ), #4342, .F. ) ;
#8615=FACE_OUTER_BOUND ( 'NONE', #12213, .T. ) ;
#8645=CARTESIAN_POINT ( 'NONE',  ( -57.72085481156722864, 1.184343223768590914, 3.558065644182727194 ) ) ;
#8664=CARTESIAN_POINT ( 'NONE',  ( -59.29999999999997584, 2.330309927981285032E-15, 4.253626757584724400E-16 ) ) ;
#8666=CARTESIAN_POINT ( 'NONE',  ( -58.17292740578360366, 2.256877952708275181, -2.542931754211918971 ) ) ;
#8679=EDGE_LOOP ( 'NONE', ( #12304, #2976, #244, #8584 ) ) ;
#8686=CARTESIAN_POINT ( 'NONE',  ( -57.79792740578359656, -2.256877952708263635, 2.542931754211924744 ) ) ;
#8704=CARTESIAN_POINT ( 'NONE',  ( -54.50000000000000000, 3.067956443743977690, -1.885759217255443376 ) ) ;
#8724=ORIENTED_EDGE ( 'NONE', *, *, #27305, .F. ) ;
#8725=DIRECTION ( 'NONE',  ( 1.000000000000000000, 3.054025858079668409E-16, -2.042474015755241579E-16 ) ) ;
#8739=CARTESIAN_POINT ( 'NONE',  ( -71.44781903063172024, -0.2962147058074217632, 1.444404304980893006 ) ) ;
#8758=DIRECTION ( 'NONE',  ( 0.000000000000000000, 0.2008964009354148039, -0.9796124928211140670 ) ) ;
#8779=CARTESIAN_POINT ( 'NONE',  ( -59.15835481156722864, -0.7533615035078041755, 3.673546848079178861 ) ) ;
#8788=CARTESIAN_POINT ( 'NONE',  ( -58.28335481156722864, -4.108500314926510022, 1.367561758111407677 ) ) ;
#8808=TOROIDAL_SURFACE ( 'NONE', #15884, 1.524417381223824197, 0.05000000000000000278 ) ;
#8815=CARTESIAN_POINT ( 'NONE',  ( -55.98542740578360366, 0.7887156198831754006, -3.845940847736172508 ) ) ;
#8834=CARTESIAN_POINT ( 'NONE',  ( -57.92292740578360366, 1.073804522883521795, 3.225979517392336682 ) ) ;
#8870=CARTESIAN_POINT ( 'NONE',  ( -60.49999999999995737, 0.8638545240222846866, -4.212333719130787912 ) ) ;
#8907=VERTEX_POINT ( 'NONE', #23600 ) ;
#8920=CARTESIAN_POINT ( 'NONE',  ( -57.77499999999997016, -0.9643027244899882167, 4.702139965541347166 ) ) ;
#8928=AXIS2_PLACEMENT_3D ( 'NONE', #11231, #20906, #23909 ) ;
#8940=AXIS2_PLACEMENT_3D ( 'NONE', #18799, #1835, #23857 ) ;
#8961=CARTESIAN_POINT ( 'NONE',  ( -57.53335481156722864, -4.108500314926510022, 1.367561758111407455 ) ) ;
#8973=ORIENTED_EDGE ( 'NONE', *, *, #13599, .T. ) ;
#8979=EDGE_CURVE ( 'NONE', #25687, #5427, #6912, .T. ) ;
#8992=CARTESIAN_POINT ( 'NONE',  ( -57.86042740578360366, -0.7887156198831708487, 3.845940847736171619 ) ) ;
#8996=ADVANCED_FACE ( 'NONE', ( #4587 ), #14237, .T. ) ;
#9014=CARTESIAN_POINT ( 'NONE',  ( -60.98542740578359656, 2.936324665650206445, 2.606018187048499968 ) ) ;
#9016=PLANE ( 'NONE',  #20844 ) ;
#9018=AXIS2_PLACEMENT_3D ( 'NONE', #25987, #9060, #11596 ) ;
#9020=DIRECTION ( 'NONE',  ( 1.000000000000000000, 3.054025858079668409E-16, -2.042474015755241579E-16 ) ) ;
#9046=VERTEX_POINT ( 'NONE', #22752 ) ;
#9050=ORIENTED_EDGE ( 'NONE', *, *, #22961, .F. ) ;
#9060=DIRECTION ( 'NONE',  ( 0.000000000000000000, 0.000000000000000000, 1.000000000000000000 ) ) ;
#9061=EDGE_LOOP ( 'NONE', ( #22741, #4407, #19095, #28880 ) ) ;
#9062=ORIENTED_EDGE ( 'NONE', *, *, #12693, .T. ) ;
#9084=CARTESIAN_POINT ( 'NONE',  ( -59.29999999999997584, 0.7533615035078071731, -3.673546848079177529 ) ) ;
#9091=VERTEX_POINT ( 'NONE', #19327 ) ;
#9095=ORIENTED_EDGE ( 'NONE', *, *, #28384, .T. ) ;
#9099=ORIENTED_EDGE ( 'NONE', *, *, #26051, .F. ) ;
#9107=CARTESIAN_POINT ( 'NONE',  ( -55.03335481156724995, 0.7533615035078067290, -3.673546848079180194 ) ) ;
#9125=DIRECTION ( 'NONE',  ( 0.000000000000000000, 0.2008964009354147484, -0.9796124928211138450 ) ) ;
#9134=CARTESIAN_POINT ( 'NONE',  ( -55.97085481156723574, -3.673546848079175309, -0.7533615035078069511 ) ) ;
#9141=ADVANCED_FACE ( 'NONE', ( #16239 ), #25564, .F. ) ;
#9156=FACE_OUTER_BOUND ( 'NONE', #11740, .T. ) ;
#9158=CARTESIAN_POINT ( 'NONE',  ( -55.61042740578360366, -0.7887156198831609677, 3.845940847736172952 ) ) ;
#9161=ADVANCED_FACE ( 'NONE', ( #25733 ), #31206, .F. ) ;
#9168=VERTEX_POINT ( 'NONE', #13826 ) ;
#9182=CARTESIAN_POINT ( 'NONE',  ( -56.12499999999997868, 2.489203624310591056, -2.804704140674918023 ) ) ;
#9183=CARTESIAN_POINT ( 'NONE',  ( -54.55048689473264290, -3.664629505757012851, 1.761501643209058221 ) ) ;
#9227=VERTEX_POINT ( 'NONE', #19098 ) ;
#9234=CARTESIAN_POINT ( 'NONE',  ( -59.96464466094062828, 2.127325729886550933E-15, 5.611146207266455330E-16 ) ) ;
#9274=CARTESIAN_POINT ( 'NONE',  ( -55.43749999999997868, 0.7533615035078096156, -3.673546848079177529 ) ) ;
#9288=CARTESIAN_POINT ( 'NONE',  ( -55.36042740578360366, -2.936324665650200672, -2.606018187048498191 ) ) ;
#9311=CARTESIAN_POINT ( 'NONE',  ( -58.29792740578360366, -1.073804522883506030, -3.225979517392338902 ) ) ;
#9331=CARTESIAN_POINT ( 'NONE',  ( -55.68749999999997868, -4.108500314926507357, 1.367561758111405901 ) ) ;
#9334=FACE_OUTER_BOUND ( 'NONE', #7037, .T. ) ;
#9341=ORIENTED_EDGE ( 'NONE', *, *, #22679, .F. ) ;
#9342=CARTESIAN_POINT ( 'NONE',  ( -57.18749999999995737, -4.108500314926507357, 1.367561758111402348 ) ) ;
#9345=TOROIDAL_SURFACE ( 'NONE', #31070, 3.250821294908289971, 0.05000000000000000278 ) ;
#9361=LINE ( 'NONE', #19026, #8452 ) ;
#9362=VERTEX_POINT ( 'NONE', #24903 ) ;
#9368=CIRCLE ( 'NONE', #17448, 0.04999999999999987094 ) ;
#9373=EDGE_CURVE ( 'NONE', #709, #23231, #3224, .T. ) ;
#9380=CARTESIAN_POINT ( 'NONE',  ( -57.43749999999997158, 3.238593381231836155, 2.874284765127032681 ) ) ;
#9411=ORIENTED_EDGE ( 'NONE', *, *, #4035, .F. ) ;
#9415=VERTEX_POINT ( 'NONE', #10195 ) ;
#9416=CARTESIAN_POINT ( 'NONE',  ( -68.01382336603234080, -3.309142602788800391E-16, 2.205138456058669928E-15 ) ) ;
#9420=CIRCLE ( 'NONE', #12913, 4.849999999999999645 ) ;
#9448=( BOUNDED_CURVE ( )  B_SPLINE_CURVE ( 2, ( #18382, #2060, #4118, #25654, #19016, #21400, #31026, #28670, #3961 ),
 .UNSPECIFIED., .F., .T. ) 
 B_SPLINE_CURVE_WITH_KNOTS ( ( 3, 2, 2, 2, 3 ),
 ( 0.1388888888888888951, 0.1481481481481481399, 0.1666666666666666574, 0.1851851851851851749, 0.1944444444444444475 ),
 .UNSPECIFIED. ) 
 CURVE ( )  GEOMETRIC_REPRESENTATION_ITEM ( )  RATIONAL_B_SPLINE_CURVE ( ( 0.9330127018922192983, 0.9330127018922194093, 1.000000000000000000, 0.8660254037844387076, 1.000000000000000000, 0.8660254037844387076, 1.000000000000000000, 0.9330127018922191873, 0.9330127018922192983 ) ) 
 REPRESENTATION_ITEM ( '' )  );
#9453=CARTESIAN_POINT ( 'NONE',  ( -55.17292740578361077, 2.256877952708269408, -2.542931754211925632 ) ) ;
#9468=CARTESIAN_POINT ( 'NONE',  ( -59.29999999999997584, 2.330309927981285032E-15, 4.253626757584724400E-16 ) ) ;
#9508=CARTESIAN_POINT ( 'NONE',  ( -55.62499999999997158, -3.673546848079173976, -0.7533615035078066180 ) ) ;
#9536=CARTESIAN_POINT ( 'NONE',  ( -59.15835481156722864, -0.7533615035078041755, 3.673546848079178861 ) ) ;
#9550=EDGE_CURVE ( 'NONE', #5992, #3096, #15580, .T. ) ;
#9562=CARTESIAN_POINT ( 'NONE',  ( -58.22085481156723574, -3.673546848079176197, -0.7533615035078065070 ) ) ;
#9565=CARTESIAN_POINT ( 'NONE',  ( -57.68749999999996447, 0.7533615035078072841, -3.673546848079177085 ) ) ;
#9570=VERTEX_POINT ( 'NONE', #1156 ) ;
#9616=CARTESIAN_POINT ( 'NONE',  ( -55.54792740578360366, -2.256877952708263191, 2.542931754211924300 ) ) ;
#9657=AXIS2_PLACEMENT_3D ( 'NONE', #23433, #1569, #16309 ) ;
#9662=CARTESIAN_POINT ( 'NONE',  ( -56.31249999999997868, -3.238593381231840151, -2.874284765127021579 ) ) ;
#9677=CARTESIAN_POINT ( 'NONE',  ( -56.81249999999997158, 4.108500314926514463, -1.367561758111402348 ) ) ;
#9692=DIRECTION ( 'NONE',  ( -1.000000000000000000, -3.054025858079668409E-16, 2.042474015755241579E-16 ) ) ;
#9696=CARTESIAN_POINT ( 'NONE',  ( -60.24999999999997868, -0.6177564328763985868, 3.012308415424926444 ) ) ;
#9697=ORIENTED_EDGE ( 'NONE', *, *, #13505, .T. ) ;
#9701=EDGE_CURVE ( 'NONE', #709, #12762, #16637, .T. ) ;
#9707=CARTESIAN_POINT ( 'NONE',  ( -58.40835481156724285, -0.7533615035077920741, 3.673546848079180638 ) ) ;
#9711=CARTESIAN_POINT ( 'NONE',  ( -54.49999999999997868, -0.7533615035078020661, 3.673546848079177085 ) ) ;
#9739=DIRECTION ( 'NONE',  ( 0.000000000000000000, -0.2008964009354147484, 0.9796124928211139560 ) ) ;
#9748=ADVANCED_FACE ( 'NONE', ( #344 ), #5941, .T. ) ;
#9750=VERTEX_POINT ( 'NONE', #24265 ) ;
#9755=CARTESIAN_POINT ( 'NONE',  ( -54.98542740578361077, 2.936324665650207333, 2.606018187048498191 ) ) ;
#9759=EDGE_CURVE ( 'NONE', #11263, #3318, #5351, .T. ) ;
#9760=CARTESIAN_POINT ( 'NONE',  ( -71.44999999999998863, -1.380331489585512972E-15, 2.906968604901091669E-15 ) ) ;
#9767=CARTESIAN_POINT ( 'NONE',  ( -71.49999999999998579, -1.395601618875910821E-15, 2.917180974979867506E-15 ) ) ;
#9796=CARTESIAN_POINT ( 'NONE',  ( -58.74999999999997158, -2.489203624310586171, 2.804704140674917134 ) ) ;
#9799=CARTESIAN_POINT ( 'NONE',  ( -56.15835481156722864, -0.7533615035077977362, 3.673546848079179750 ) ) ;
#9832=FACE_OUTER_BOUND ( 'NONE', #14252, .T. ) ;
#9839=EDGE_CURVE ( 'NONE', #13554, #5591, #3410, .T. ) ;
#9844=DIRECTION ( 'NONE',  ( 0.9992009587217894895, 0.008029435056737248277, -0.03915318968010821771 ) ) ;
#9859=FACE_OUTER_BOUND ( 'NONE', #2051, .T. ) ;
#9863=EDGE_CURVE ( 'NONE', #20313, #4537, #18661, .T. ) ;
#9864=VERTEX_POINT ( 'NONE', #9799 ) ;
#9870=CARTESIAN_POINT ( 'NONE',  ( -59.96464466094062828, -0.9714054848608590920, 4.736774497371793125 ) ) ;
#9889=VECTOR ( 'NONE', #28421, 1000.000000000000000 ) ;
#9904=CARTESIAN_POINT ( 'NONE',  ( -60.34585481156722864, -1.184343223768586695, -3.558065644182724974 ) ) ;
#9906=DIRECTION ( 'NONE',  ( 0.9992009587217894895, -0.008029435056736641124, 0.03915318968010780831 ) ) ;
#9909=ORIENTED_EDGE ( 'NONE', *, *, #17370, .T. ) ;
#9921=TOROIDAL_SURFACE ( 'NONE', #14966, 4.800000000000000711, 0.05000000000000000278 ) ;
#9925=AXIS2_PLACEMENT_3D ( 'NONE', #26480, #13541, #25573 ) ;
#9957=CARTESIAN_POINT ( 'NONE',  ( -57.56249999999997868, 4.108500314926511798, -1.367561758111407455 ) ) ;
#9963=CARTESIAN_POINT ( 'NONE',  ( -54.49999999999997868, 0.2900967345938421649, -3.387601494358211340 ) ) ;
#9976=CARTESIAN_POINT ( 'NONE',  ( -59.29999999999997584, 0.7533615035078071731, -3.673546848079177529 ) ) ;
#9982=ADVANCED_FACE ( 'NONE', ( #9334 ), #20099, .F. ) ;
#10004=EDGE_CURVE ( 'NONE', #1074, #6162, #14843, .T. ) ;
#10009=AXIS2_PLACEMENT_3D ( 'NONE', #29232, #5299, #14957 ) ;
#10023=DIRECTION ( 'NONE',  ( -1.000000000000000000, -3.054025858079668409E-16, 2.042474015755241579E-16 ) ) ;
#10027=CARTESIAN_POINT ( 'NONE',  ( -57.77499999999997016, 0.9643027244899933237, -4.702139965541347166 ) ) ;
#10064=CARTESIAN_POINT ( 'NONE',  ( -57.79792740578359656, -2.256877952708263635, 2.542931754211924744 ) ) ;
#10111=CARTESIAN_POINT ( 'NONE',  ( -59.43749999999997158, -4.108500314926507357, 1.367561758111406789 ) ) ;
#10114=CIRCLE ( 'NONE', #8079, 1.524417381223824197 ) ;
#10136=CARTESIAN_POINT ( 'NONE',  ( -71.44999999999998863, 0.2962051453644842236, -1.444357686279446273 ) ) ;
#10138=ORIENTED_EDGE ( 'NONE', *, *, #10004, .T. ) ;
#10144=( BOUNDED_CURVE ( )  B_SPLINE_CURVE ( 2, ( #5364, #22175, #161, #19792, #19482, #9677, #29426, #15025, #24686 ),
 .UNSPECIFIED., .F., .T. ) 
 B_SPLINE_CURVE_WITH_KNOTS ( ( 3, 2, 2, 2, 3 ),
 ( 0.3055555555555555802, 0.3148148148148148251, 0.3333333333333333148, 0.3518518518518518601, 0.3611111111111111605 ),
 .UNSPECIFIED. ) 
 CURVE ( )  GEOMETRIC_REPRESENTATION_ITEM ( )  RATIONAL_B_SPLINE_CURVE ( ( 0.9330127018922194093, 0.9330127018922195203, 1.000000000000000000, 0.8660254037844387076, 1.000000000000000000, 0.8660254037844387076, 1.000000000000000000, 0.9330127018922189652, 0.9330127018922194093 ) ) 
 REPRESENTATION_ITEM ( '' )  );
#10148=CARTESIAN_POINT ( 'NONE',  ( -59.29999999999996874, -2.718478022535892880, -2.574424139164518621 ) ) ;
#10157=DIRECTION ( 'NONE',  ( 0.000000000000000000, -0.2008964009354162750, 0.9796124928211136229 ) ) ;
#10178=CARTESIAN_POINT ( 'NONE',  ( -60.54999999999995453, 0.7328781032566589193, -3.573665542649862914 ) ) ;
#10179=ORIENTED_EDGE ( 'NONE', *, *, #6839, .T. ) ;
#10187=CIRCLE ( 'NONE', #18294, 0.04999999999999988481 ) ;
#10195=CARTESIAN_POINT ( 'NONE',  ( -68.01382336603234080, -0.6601810586021509275, 3.219179684251519458 ) ) ;
#10204=CIRCLE ( 'NONE', #1604, 3.075000000000000622 ) ;
#10209=CARTESIAN_POINT ( 'NONE',  ( -58.92292740578360366, 2.256877952708268964, -2.542931754211924744 ) ) ;
#10239=CARTESIAN_POINT ( 'NONE',  ( -59.29999999999998295, 2.957953439200568635, 2.295354275992711024 ) ) ;
#10243=DIRECTION ( 'NONE',  ( 0.000000000000000000, -0.2008964009354147484, 0.9796124928211139560 ) ) ;
#10246=CARTESIAN_POINT ( 'NONE',  ( -55.03335481156724285, 0.8699069336946695374, -4.241846523238430144 ) ) ;
#10259=CARTESIAN_POINT ( 'NONE',  ( -59.31249999999997158, -3.238593381231841040, -2.874284765127020247 ) ) ;
#10267=EDGE_LOOP ( 'NONE', ( #22232, #9095 ) ) ;
#10275=CARTESIAN_POINT ( 'NONE',  ( -59.29999999999997584, -0.7533615035078030653, 3.673546848079178417 ) ) ;
#10293=DIRECTION ( 'NONE',  ( 2.614375865348240525E-16, -0.2008964009354147762, 0.9796124928211140670 ) ) ;
#10311=FACE_OUTER_BOUND ( 'NONE', #29203, .T. ) ;
#10329=SHAPE_REPRESENTATION_RELATIONSHIP ( 'NONE' , 'NONE' ,  #3777, #1717 ) ;
#10351=CARTESIAN_POINT ( 'NONE',  ( -56.72499999999997300, 3.116721586436802063E-15, -1.005743832985040150E-16 ) ) ;
#10359=CARTESIAN_POINT ( 'NONE',  ( -54.49999999999997868, 0.2900967345938421649, -3.387601494358211340 ) ) ;
#10360=CARTESIAN_POINT ( 'NONE',  ( -57.73542740578360366, -3.725040285533365303, 1.239922660687675204 ) ) ;
#10367=EDGE_LOOP ( 'NONE', ( #6244, #1929, #1520, #27753 ) ) ;
#10371=CIRCLE ( 'NONE', #16430, 0.04999999999999989175 ) ;
#10383=EDGE_CURVE ( 'NONE', #6063, #4965, #6377, .T. ) ;
#10402=CARTESIAN_POINT ( 'NONE',  ( -55.15835481156724285, -3.238593381231841928, -2.874284765127022911 ) ) ;
#10414=CARTESIAN_POINT ( 'NONE',  ( -59.12499999999997158, 2.489203624310590612, -2.804704140674917134 ) ) ;
#10419=CARTESIAN_POINT ( 'NONE',  ( -54.49999999999995737, -2.900697337314245505, -2.163606381124719924 ) ) ;
#10431=CARTESIAN_POINT ( 'NONE',  ( -54.98542740578361077, 2.936324665650207333, 2.606018187048498191 ) ) ;
#10440=CONICAL_SURFACE ( 'NONE', #13947, 2.099999999999999645, 0.7853981633974396193 ) ;
#10453=VERTEX_POINT ( 'NONE', #20310 ) ;
#10473=DIRECTION ( 'NONE',  ( 1.000000000000000000, 3.054025858079668409E-16, -2.042474015755241579E-16 ) ) ;
#10482=CARTESIAN_POINT ( 'NONE',  ( -54.49999999999999289, 1.970152530825497017, -2.913597794826568332 ) ) ;
#10496=ORIENTED_EDGE ( 'NONE', *, *, #28790, .F. ) ;
#10509=AXIS2_PLACEMENT_3D ( 'NONE', #26750, #4721, #16630 ) ;
#10518=DIRECTION ( 'NONE',  ( 1.000000000000000000, 3.054025858079668409E-16, -2.042474015755241579E-16 ) ) ;
#10520=EDGE_CURVE ( 'NONE', #26980, #5427, #26443, .T. ) ;
#10527=DIRECTION ( 'NONE',  ( -2.614375865348240525E-16, 0.2008964009354147484, -0.9796124928211139560 ) ) ;
#10534=CARTESIAN_POINT ( 'NONE',  ( -57.11042740578361077, -0.7887156198831601905, 3.845940847736173840 ) ) ;
#10539=CARTESIAN_POINT ( 'NONE',  ( -55.78335481156724285, 0.7533615035078067290, -3.673546848079180194 ) ) ;
#10545=CARTESIAN_POINT ( 'NONE',  ( -67.99999999999995737, 0.6629581230868679675, -3.232721226309673845 ) ) ;
#10566=EDGE_CURVE ( 'NONE', #12762, #11632, #22015, .T. ) ;
#10568=ORIENTED_EDGE ( 'NONE', *, *, #26030, .F. ) ;
#10600=TOROIDAL_SURFACE ( 'NONE', #14647, 2.150000000000000355, 0.05000000000000000278 ) ;
#10609=CARTESIAN_POINT ( 'NONE',  ( -57.31249999999996447, -0.7533615035078060629, 3.673546848079176641 ) ) ;
#10613=CARTESIAN_POINT ( 'NONE',  ( -57.11042740578361077, -0.7887156198831601905, 3.845940847736173840 ) ) ;
#10614=EDGE_CURVE ( 'NONE', #5591, #13554, #22714, .T. ) ;
#10617=CARTESIAN_POINT ( 'NONE',  ( -59.30000000000000426, -3.594491936234972318, -0.2567477776118052835 ) ) ;
#10634=CARTESIAN_POINT ( 'NONE',  ( -54.49999999999997158, 0.5440517917263103520, -3.381945888744238626 ) ) ;
#10641=CARTESIAN_POINT ( 'NONE',  ( -60.49999999999995737, -0.8638545240222812449, 4.212333719130789689 ) ) ;
#10653=EDGE_CURVE ( 'NONE', #14688, #25687, #10144, .T. ) ;
#10658=EDGE_CURVE ( 'NONE', #2983, #29380, #18170, .T. ) ;
#10680=CARTESIAN_POINT ( 'NONE',  ( -58.67292740578360366, 1.073804522883521351, 3.225979517392336682 ) ) ;
#10726=AXIS2_PLACEMENT_3D ( 'NONE', #9468, #21676, #19134 ) ;
#10735=CIRCLE ( 'NONE', #3724, 0.5000000000000013323 ) ;
#10743=ORIENTED_EDGE ( 'NONE', *, *, #15038, .F. ) ;
#10745=ORIENTED_EDGE ( 'NONE', *, *, #11947, .T. ) ;
#10747=FACE_OUTER_BOUND ( 'NONE', #18723, .T. ) ;
#10758=CARTESIAN_POINT ( 'NONE',  ( -57.73542740578360366, -3.725040285533365303, 1.239922660687675204 ) ) ;
#10759=CIRCLE ( 'NONE', #14797, 4.314644660940672338 ) ;
#10769=FACE_OUTER_BOUND ( 'NONE', #206, .T. ) ;
#10772=AXIS2_PLACEMENT_3D ( 'NONE', #12493, #27520, #20122 ) ;
#10785=DIRECTION ( 'NONE',  ( 0.7071067811865487940, -0.1420552074174027679, 0.6926906366088665390 ) ) ;
#10808=( BOUNDED_CURVE ( )  B_SPLINE_CURVE ( 2, ( #9565, #30761, #30920, #6691, #16685, #25999, #28538, #16353, #30586 ),
 .UNSPECIFIED., .F., .T. ) 
 B_SPLINE_CURVE_WITH_KNOTS ( ( 3, 2, 2, 2, 3 ),
 ( 0.4722222222222222654, 0.4814814814814814548, 0.5000000000000000000, 0.5185185185185184897, 0.5277777777777777901 ),
 .UNSPECIFIED. ) 
 CURVE ( )  GEOMETRIC_REPRESENTATION_ITEM ( )  RATIONAL_B_SPLINE_CURVE ( ( 0.9330127018922194093, 0.9330127018922197424, 1.000000000000000000, 0.8660254037844387076, 1.000000000000000000, 0.8660254037844387076, 1.000000000000000000, 0.9330127018922194093, 0.9330127018922194093 ) ) 
 REPRESENTATION_ITEM ( '' )  );
#10834=AXIS2_PLACEMENT_3D ( 'NONE', #23106, #1398, #11058 ) ;
#10850=CARTESIAN_POINT ( 'NONE',  ( -58.44184846062113081, 0.2309624077929140484, 3.875409454552789956 ) ) ;
#10860=ORIENTED_EDGE ( 'NONE', *, *, #18558, .T. ) ;
#10863=CIRCLE ( 'NONE', #6325, 3.750000000000000444 ) ;
#10874=AXIS2_PLACEMENT_3D ( 'NONE', #24705, #3017, #10293 ) ;
#10889=CONICAL_SURFACE ( 'NONE', #3792, 3.299999999999999822, 0.03997868712329010615 ) ;
#10890=CYLINDRICAL_SURFACE ( 'NONE', #802, 4.849999999999999645 ) ;
#10910=CARTESIAN_POINT ( 'NONE',  ( -55.65835481156724285, 4.108500314926515351, -1.367561758111408565 ) ) ;
#10911=CARTESIAN_POINT ( 'NONE',  ( -57.54792740578359656, -1.073804522883517132, -3.225979517392335350 ) ) ;
#10926=EDGE_CURVE ( 'NONE', #11953, #5317, #6508, .T. ) ;
#10930=EDGE_CURVE ( 'NONE', #23943, #29251, #17147, .T. ) ;
#10960=CARTESIAN_POINT ( 'NONE',  ( -59.29999999999997584, 2.330309927981285032E-15, 4.253626757584724400E-16 ) ) ;
#10967=AXIS2_PLACEMENT_3D ( 'NONE', #9234, #21128, #28231 ) ;
#10987=CARTESIAN_POINT ( 'NONE',  ( -59.29999999999996874, -0.4436653460577585362, 3.502232364094418848 ) ) ;
#11010=( BOUNDED_CURVE ( )  B_SPLINE_CURVE ( 2, ( #8314, #17986, #27635, #3578, #22898, #11017, #18625, #28424, #16558 ),
 .UNSPECIFIED., .F., .T. ) 
 B_SPLINE_CURVE_WITH_KNOTS ( ( 3, 2, 2, 2, 3 ),
 ( 0.5277777777777777901, 0.5370370370370370905, 0.5555555555555555802, 0.5740740740740740700, 0.5833333333333333703 ),
 .UNSPECIFIED. ) 
 CURVE ( )  GEOMETRIC_REPRESENTATION_ITEM ( )  RATIONAL_B_SPLINE_CURVE ( ( 0.9330127018922194093, 0.9330127018922194093, 1.000000000000000000, 0.8660254037844387076, 1.000000000000000000, 0.8660254037844387076, 1.000000000000000000, 0.9330127018922189652, 0.9330127018922194093 ) ) 
 REPRESENTATION_ITEM ( '' )  );
#11017=CARTESIAN_POINT ( 'NONE',  ( -57.90835481156723574, 4.108500314926515351, -1.367561758111408121 ) ) ;
#11026=CARTESIAN_POINT ( 'NONE',  ( -59.09585481156723574, -2.489203624310587504, 2.804704140674918911 ) ) ;
#11030=CARTESIAN_POINT ( 'NONE',  ( -59.18749999999996447, 0.7533615035078157218, -3.673546848079175309 ) ) ;
#11035=CARTESIAN_POINT ( 'NONE',  ( -58.97085481156723574, -3.673546848079176197, -0.7533615035078063960 ) ) ;
#11039=CARTESIAN_POINT ( 'NONE',  ( -71.44999999999998863, 0.4118376219175989839, -2.008205610283281040 ) ) ;
#11042=CARTESIAN_POINT ( 'NONE',  ( -60.49999999999995737, 1.963826825011730345E-15, 6.704595576490977020E-16 ) ) ;
#11050=SURFACE_STYLE_FILL_AREA ( #4076 ) ;
#11055=CARTESIAN_POINT ( 'NONE',  ( -57.73542740578359656, -3.725040285533367079, 1.239922660687670097 ) ) ;
#11057=CARTESIAN_POINT ( 'NONE',  ( -56.53335481156723574, 0.7533615035078095046, -3.673546848079178861 ) ) ;
#11058=DIRECTION ( 'NONE',  ( 0.000000000000000000, -0.2008964009354147484, 0.9796124928211139560 ) ) ;
#11075=CARTESIAN_POINT ( 'NONE',  ( -55.73542740578360366, 2.936324665650206889, 2.606018187048498191 ) ) ;
#11090=DIRECTION ( 'NONE',  ( -1.000000000000000000, -3.054025858079668409E-16, 2.042474015755241579E-16 ) ) ;
#11095=ORIENTED_EDGE ( 'NONE', *, *, #15831, .T. ) ;
#11097=CARTESIAN_POINT ( 'NONE',  ( -59.92928932188130631, 2.138123341857387114E-15, 5.538933845919563674E-16 ) ) ;
#11104=VERTEX_POINT ( 'NONE', #21140 ) ;
#11112=AXIS2_PLACEMENT_3D ( 'NONE', #29403, #31321, #7715 ) ;
#11113=ADVANCED_FACE ( 'NONE', ( #4318 ), #28781, .T. ) ;
#11125=ADVANCED_FACE ( 'NONE', ( #21300 ), #31303, .T. ) ;
#11131=CARTESIAN_POINT ( 'NONE',  ( -55.77900635094609072, -1.737685414808515016, 3.471684241605562438 ) ) ;
#11133=CARTESIAN_POINT ( 'NONE',  ( -54.54999999999998295, 3.780972210569126836E-15, -5.448124817252668230E-16 ) ) ;
#11144=ORIENTED_EDGE ( 'NONE', *, *, #2726, .T. ) ;
#11163=DIRECTION ( 'NONE',  ( 1.000000000000000000, 3.054025858079668409E-16, -2.042474015755241579E-16 ) ) ;
#11176=CARTESIAN_POINT ( 'NONE',  ( -59.12499999999997158, 2.489203624310598162, -2.804704140674910473 ) ) ;
#11183=CARTESIAN_POINT ( 'NONE',  ( -56.72085481156723574, -3.673546848079175753, -0.7533615035078068400 ) ) ;
#11188=DIRECTION ( 'NONE',  ( 0.000000000000000000, 0.2008964009354147484, -0.9796124928211139560 ) ) ;
#11199=SURFACE_SIDE_STYLE ('',( #11050 ) ) ;
#11205=CARTESIAN_POINT ( 'NONE',  ( -57.29792740578360366, 3.330682475591789427, 0.6830477631804139360 ) ) ;
#11215=CARTESIAN_POINT ( 'NONE',  ( -57.72499999999997300, 2.811319000628834039E-15, 1.036730182770210180E-16 ) ) ;
#11224=CARTESIAN_POINT ( 'NONE',  ( -58.98542740578360366, 0.7887156198831661857, -3.845940847736173840 ) ) ;
#11231=CARTESIAN_POINT ( 'NONE',  ( -71.49999999999998579, -1.395601618875910821E-15, 2.917180974979867506E-15 ) ) ;
#11237=CARTESIAN_POINT ( 'NONE',  ( -54.68749999999997868, 0.7533615035078081723, -3.673546848079177973 ) ) ;
#11238=DIRECTION ( 'NONE',  ( 1.000000000000000000, 3.054025858079668409E-16, -2.042474015755241579E-16 ) ) ;
#11256=CARTESIAN_POINT ( 'NONE',  ( -56.72499999999997300, 0.9241234443029111567, -4.506217466977124886 ) ) ;
#11260=EDGE_CURVE ( 'NONE', #10453, #23943, #27279, .T. ) ;
#11263=VERTEX_POINT ( 'NONE', #13157 ) ;
#11288=ORIENTED_EDGE ( 'NONE', *, *, #16689, .F. ) ;
#11289=AXIS2_PLACEMENT_3D ( 'NONE', #7951, #17616, #22515 ) ;
#11307=DIRECTION ( 'NONE',  ( 0.000000000000000000, -0.2008964009354147484, 0.9796124928211139560 ) ) ;
#11317=ORIENTED_EDGE ( 'NONE', *, *, #7724, .F. ) ;
#11325=CARTESIAN_POINT ( 'NONE',  ( -56.59585481156723574, -1.184343223768586251, -3.558065644182725862 ) ) ;
#11357=AXIS2_PLACEMENT_3D ( 'NONE', #12770, #17859, #27497 ) ;
#11371=ORIENTED_EDGE ( 'NONE', *, *, #3615, .F. ) ;
#11378=CARTESIAN_POINT ( 'NONE',  ( -54.87499999999997868, -3.673546848079173532, -0.7533615035078067290 ) ) ;
#11386=EDGE_CURVE ( 'NONE', #29844, #6742, #2220, .T. ) ;
#11403=AXIS2_PLACEMENT_3D ( 'NONE', #7029, #16691, #12371 ) ;
#11428=AXIS2_PLACEMENT_3D ( 'NONE', #29621, #10023, #29462 ) ;
#11450=AXIS2_PLACEMENT_3D ( 'NONE', #15415, #13187, #1160 ) ;
#11461=CARTESIAN_POINT ( 'NONE',  ( -60.98542740578359656, 2.936324665650206445, 2.606018187048499968 ) ) ;
#11507=CARTESIAN_POINT ( 'NONE',  ( -55.84585481156723574, -1.184343223768586029, -3.558065644182725862 ) ) ;
#11520=FACE_OUTER_BOUND ( 'NONE', #7499, .T. ) ;
#11521=VERTEX_POINT ( 'NONE', #10136 ) ;
#11530=CARTESIAN_POINT ( 'NONE',  ( -56.49986116251334778, 1.737685414808521678, -3.471684241605565546 ) ) ;
#11532=CIRCLE ( 'NONE', #1418, 3.286176633967618166 ) ;
#11533=CARTESIAN_POINT ( 'NONE',  ( -56.79792740578360366, -1.073804522883507140, -3.225979517392339346 ) ) ;
#11550=DIRECTION ( 'NONE',  ( -1.000000000000000000, -3.054025858079668409E-16, 2.042474015755241579E-16 ) ) ;
#11556=CARTESIAN_POINT ( 'NONE',  ( -56.74999999999997158, 3.673546848079180638, 0.7533615035078058408 ) ) ;
#11577=AXIS2_PLACEMENT_3D ( 'NONE', #19379, #4958, #14611 ) ;
#11593=VERTEX_POINT ( 'NONE', #13410 ) ;
#11596=DIRECTION ( 'NONE',  ( 1.000000000000000000, 0.000000000000000000, 0.000000000000000000 ) ) ;
#11624=VERTEX_POINT ( 'NONE', #3941 ) ;
#11632=VERTEX_POINT ( 'NONE', #15510 ) ;
#11648=CARTESIAN_POINT ( 'NONE',  ( -57.77499999999997016, -0.9743475445367594245, 4.751120590182401848 ) ) ;
#11663=CARTESIAN_POINT ( 'NONE',  ( -55.47085481156723574, 1.184343223768591580, 3.558065644182726750 ) ) ;
#11684=DIRECTION ( 'NONE',  ( 0.000000000000000000, 0.2008964009354162750, -0.9796124928211136229 ) ) ;
#11685=CARTESIAN_POINT ( 'NONE',  ( -57.92292740578360366, 1.073804522883512691, 3.225979517392339346 ) ) ;
#11692=EDGE_CURVE ( 'NONE', #9227, #2190, #2522, .T. ) ;
#11705=CARTESIAN_POINT ( 'NONE',  ( -60.54792740578359656, -1.073804522883517576, -3.225979517392334905 ) ) ;
#11719=DIRECTION ( 'NONE',  ( 1.000000000000000000, 3.054025858079668409E-16, -2.042474015755241579E-16 ) ) ;
#11740=EDGE_LOOP ( 'NONE', ( #14276, #20668, #11095, #30661 ) ) ;
#11748=EDGE_LOOP ( 'NONE', ( #25935, #14443, #13208, #16703 ) ) ;
#11790=CYLINDRICAL_SURFACE ( 'NONE', #5671, 3.750000000000000444 ) ;
#11812=CARTESIAN_POINT ( 'NONE',  ( -56.54792740578360366, 3.330682475591790315, 0.6830477631804106053 ) ) ;
#11836=( BOUNDED_CURVE ( )  B_SPLINE_CURVE ( 2, ( #18974, #2168, #26547, #26402, #6767, #14353, #13866, #11530, #21363 ),
 .UNSPECIFIED., .F., .T. ) 
 B_SPLINE_CURVE_WITH_KNOTS ( ( 3, 2, 2, 2, 3 ),
 ( 0.3055555555555555802, 0.3148148148148148251, 0.3333333333333333148, 0.3518518518518518601, 0.3611111111111111049 ),
 .UNSPECIFIED. ) 
 CURVE ( )  GEOMETRIC_REPRESENTATION_ITEM ( )  RATIONAL_B_SPLINE_CURVE ( ( 0.9330127018922194093, 0.9330127018922195203, 1.000000000000000000, 0.8660254037844387076, 1.000000000000000000, 0.8660254037844387076, 1.000000000000000000, 0.9330127018922194093, 0.9330127018922194093 ) ) 
 REPRESENTATION_ITEM ( '' )  );
#11855=CARTESIAN_POINT ( 'NONE',  ( -60.79792740578359656, -2.256877952708263635, 2.542931754211925188 ) ) ;
#11861=CARTESIAN_POINT ( 'NONE',  ( -59.24999999999997158, -1.184343223768572706, -3.558065644182728082 ) ) ;
#11866=CARTESIAN_POINT ( 'NONE',  ( -56.93749999999996447, 0.7533615035078061739, -3.673546848079177973 ) ) ;
#11879=ORIENTED_EDGE ( 'NONE', *, *, #9839, .F. ) ;
#11909=CARTESIAN_POINT ( 'NONE',  ( -58.06684846062112371, -0.2309624077929089692, -3.875409454552789512 ) ) ;
#11919=DIRECTION ( 'NONE',  ( 0.000000000000000000, 0.2008964009354141933, -0.9796124928211140670 ) ) ;
#11945=VECTOR ( 'NONE', #7355, 1000.000000000000114 ) ;
#11947=EDGE_CURVE ( 'NONE', #24689, #6742, #24765, .T. ) ;
#11953=VERTEX_POINT ( 'NONE', #14693 ) ;
#11957=AXIS2_PLACEMENT_3D ( 'NONE', #4612, #23632, #4459 ) ;
#11972=CARTESIAN_POINT ( 'NONE',  ( -55.98542740578361077, 0.7887156198831667409, -3.845940847736174728 ) ) ;
#11977=ORIENTED_EDGE ( 'NONE', *, *, #5080, .F. ) ;
#11990=AXIS2_PLACEMENT_3D ( 'NONE', #16619, #2517, #31002 ) ;
#12004=EDGE_LOOP ( 'NONE', ( #781, #22924, #26536, #28224 ) ) ;
#12020=VECTOR ( 'NONE', #28163, 1000.000000000000000 ) ;
#12027=CARTESIAN_POINT ( 'NONE',  ( -54.62499999999997868, 2.489203624310591501, -2.804704140674918467 ) ) ;
#12037=ADVANCED_FACE ( 'NONE', ( #15925 ), #10600, .F. ) ;
#12041=CARTESIAN_POINT ( 'NONE',  ( -69.19999999999998863, 0.4218824419643700252, -2.057186234924337054 ) ) ;
#12048=DIRECTION ( 'NONE',  ( -1.000000000000000000, -3.054025858079668409E-16, 2.042474015755241579E-16 ) ) ;
#12067=EDGE_LOOP ( 'NONE', ( #9341, #6660, #5146, #26521, #20004 ) ) ;
#12082=DIRECTION ( 'NONE',  ( 0.000000000000000000, -0.2008964009354147484, 0.9796124928211139560 ) ) ;
#12092=DIRECTION ( 'NONE',  ( -1.000000000000000000, -3.054025858079668409E-16, 2.042474015755241579E-16 ) ) ;
#12093=CARTESIAN_POINT ( 'NONE',  ( -58.87499999999997158, 1.184343223768566933, 3.558065644182732967 ) ) ;
#12131=CARTESIAN_POINT ( 'NONE',  ( -55.23542740578361077, 0.7887156198831668519, -3.845940847736174728 ) ) ;
#12155=CARTESIAN_POINT ( 'NONE',  ( -60.49999999999995737, 1.963826825011730345E-15, 6.704595576490977020E-16 ) ) ;
#12176=CARTESIAN_POINT ( 'NONE',  ( -59.62499999999997158, 1.184343223768590025, 3.558065644182725862 ) ) ;
#12201=CARTESIAN_POINT ( 'NONE',  ( -59.25776236348306014, 2.397420733123352576, 3.154278791497947765 ) ) ;
#12209=FACE_OUTER_BOUND ( 'NONE', #17576, .T. ) ;
#12211=ORIENTED_EDGE ( 'NONE', *, *, #159, .T. ) ;
#12213=EDGE_LOOP ( 'NONE', ( #24873, #22728, #21856, #8267 ) ) ;
#12222=DIRECTION ( 'NONE',  ( -2.581436205204234499E-16, 0.9796124928211140670, 0.2008964009354147762 ) ) ;
#12223=EDGE_CURVE ( 'NONE', #28004, #24689, #16887, .T. ) ;
#12244=ORIENTED_EDGE ( 'NONE', *, *, #10383, .T. ) ;
#12260=CARTESIAN_POINT ( 'NONE',  ( -54.49999999999997868, 3.796242339859525868E-15, -5.550248518040434488E-16 ) ) ;
#12270=CARTESIAN_POINT ( 'NONE',  ( -60.72085481156722864, 1.184343223768590470, 3.558065644182728082 ) ) ;
#12286=CARTESIAN_POINT ( 'NONE',  ( -56.53335481156723574, 0.7533615035078095046, -3.673546848079178861 ) ) ;
#12304=ORIENTED_EDGE ( 'NONE', *, *, #25578, .F. ) ;
#12309=CARTESIAN_POINT ( 'NONE',  ( -57.74999999999997158, -1.184343223768585807, -3.558065644182723641 ) ) ;
#12335=DIRECTION ( 'NONE',  ( 0.000000000000000000, -0.2008964009354147762, 0.9796124928211140670 ) ) ;
#12350=CARTESIAN_POINT ( 'NONE',  ( -71.44999999999998863, -0.2962051453644871657, 1.444357686279452047 ) ) ;
#12371=DIRECTION ( 'NONE',  ( -2.614375865348240525E-16, 0.2008964009354147762, -0.9796124928211140670 ) ) ;
#12375=CARTESIAN_POINT ( 'NONE',  ( -59.92928932188130631, -0.9743475445367597576, 4.751120590182403625 ) ) ;
#12380=ORIENTED_EDGE ( 'NONE', *, *, #2752, .F. ) ;
#12388=ADVANCED_FACE ( 'NONE', ( #12209 ), #13996, .T. ) ;
#12417=CARTESIAN_POINT ( 'NONE',  ( -57.54792740578359656, -1.073804522883517132, -3.225979517392335350 ) ) ;
#12423=DIRECTION ( 'NONE',  ( 1.000000000000000000, 3.054025858079668409E-16, -2.042474015755241579E-16 ) ) ;
#12430=MECHANICAL_DESIGN_GEOMETRIC_PRESENTATION_REPRESENTATION('',(#4846),#19033);
#12432=CARTESIAN_POINT ( 'NONE',  ( -58.12499999999997158, 1.184343223768580255, 3.558065644182728526 ) ) ;
#12468=CARTESIAN_POINT ( 'NONE',  ( -60.31249999999996447, -0.8699069336946629871, 4.241846523238429256 ) ) ;
#12471=CARTESIAN_POINT ( 'NONE',  ( -55.12499999999997868, 1.184343223768590692, 3.558065644182724530 ) ) ;
#12481=AXIS2_PLACEMENT_3D ( 'NONE', #14584, #2560, #27928 ) ;
#12483=CIRCLE ( 'NONE', #1871, 2.114644660940672605 ) ;
#12493=CARTESIAN_POINT ( 'NONE',  ( -71.44999999999998863, -0.4118376219176019259, 2.008205610283286813 ) ) ;
#12508=CARTESIAN_POINT ( 'NONE',  ( -55.61042740578361077, -0.7887156198831598575, 3.845940847736173840 ) ) ;
#12547=DIRECTION ( 'NONE',  ( 0.000000000000000000, -0.2008964009354162750, 0.9796124928211136229 ) ) ;
#12579=CARTESIAN_POINT ( 'NONE',  ( -60.61042740578359656, -2.936324665650201560, -2.606018187048497303 ) ) ;
#12580=FACE_OUTER_BOUND ( 'NONE', #14501, .T. ) ;
#12618=ORIENTED_EDGE ( 'NONE', *, *, #8979, .F. ) ;
#12627=CARTESIAN_POINT ( 'NONE',  ( -60.18749999999997158, -4.108500314926507357, 1.367561758111407011 ) ) ;
#12628=CARTESIAN_POINT ( 'NONE',  ( -71.49999999999998579, 0.4218824419643696921, -2.057186234924337054 ) ) ;
#12654=EDGE_CURVE ( 'NONE', #23979, #5992, #29536, .T. ) ;
#12664=FILL_AREA_STYLE_COLOUR ( '', #26751 ) ;
#12691=DIRECTION ( 'NONE',  ( 0.000000000000000000, 0.2008964009354141933, -0.9796124928211140670 ) ) ;
#12693=EDGE_CURVE ( 'NONE', #5591, #26849, #19096, .T. ) ;
#12732=CARTESIAN_POINT ( 'NONE',  ( -58.61042740578358945, -0.7887156198831605236, 3.845940847736174284 ) ) ;
#12745=EDGE_CURVE ( 'NONE', #19589, #25687, #18225, .T. ) ;
#12757=VECTOR ( 'NONE', #19317, 1000.000000000000000 ) ;
#12759=CARTESIAN_POINT ( 'NONE',  ( -59.29999999999996163, -1.164288416760277833, 3.283393033056293486 ) ) ;
#12762=VERTEX_POINT ( 'NONE', #21774 ) ;
#12770=CARTESIAN_POINT ( 'NONE',  ( -69.22071067811863543, -0.4319272620111427874, 2.106166859565398397 ) ) ;
#12772=VERTEX_POINT ( 'NONE', #19314 ) ;
#12777=CARTESIAN_POINT ( 'NONE',  ( -59.56249999999996447, -0.8699069336946628761, 4.241846523238429256 ) ) ;
#12783=CIRCLE ( 'NONE', #24918, 0.04999999999999989175 ) ;
#12809=CARTESIAN_POINT ( 'NONE',  ( -54.54792740578361077, -1.073804522883516688, -3.225979517392336238 ) ) ;
#12846=CARTESIAN_POINT ( 'NONE',  ( -71.44999999999998863, -0.3062499654112579295, 1.493338310920507839 ) ) ;
#12874=TOROIDAL_SURFACE ( 'NONE', #10874, 4.800000000000000711, 0.05000000000000000278 ) ;
#12880=CARTESIAN_POINT ( 'NONE',  ( -58.98542740578360366, 0.7887156198831661857, -3.845940847736173840 ) ) ;
#12905=CARTESIAN_POINT ( 'NONE',  ( -56.93749999999996447, 0.7533615035078061739, -3.673546848079177973 ) ) ;
#12907=CARTESIAN_POINT ( 'NONE',  ( -58.47085481156723574, 1.184343223768590692, 3.558065644182727194 ) ) ;
#12908=CIRCLE ( 'NONE', #6845, 0.04999999999999987094 ) ;
#12913=AXIS2_PLACEMENT_3D ( 'NONE', #3585, #1195, #8489 ) ;
#12929=CARTESIAN_POINT ( 'NONE',  ( -55.78335481156724285, 0.7533615035078067290, -3.673546848079180194 ) ) ;
#12951=CARTESIAN_POINT ( 'NONE',  ( -55.48542740578360366, -3.725040285533364859, 1.239922660687672540 ) ) ;
#12976=CARTESIAN_POINT ( 'NONE',  ( -55.44184846062112371, 0.2309624077929101071, 3.875409454552791733 ) ) ;
#12978=CARTESIAN_POINT ( 'NONE',  ( -56.98542740578360366, -3.725040285533364859, 1.239922660687675204 ) ) ;
#12982=CARTESIAN_POINT ( 'NONE',  ( -59.29999999999997584, -2.208048483361063852, 2.585444235547710967 ) ) ;
#12990=DIRECTION ( 'NONE',  ( 2.614375865348240525E-16, -0.2008964009354147762, 0.9796124928211140670 ) ) ;
#12999=CARTESIAN_POINT ( 'NONE',  ( -71.44999999999998863, 0.3062499654112550429, -1.493338310920502066 ) ) ;
#13028=VECTOR ( 'NONE', #25893, 1000.000000000000114 ) ;
#13040=PLANE ( 'NONE',  #8327 ) ;
#13052=CARTESIAN_POINT ( 'NONE',  ( -58.73542740578359656, 2.936324665650206889, 2.606018187048499080 ) ) ;
#13074=CARTESIAN_POINT ( 'NONE',  ( -58.74986116251333357, 1.737685414808516793, -3.471684241605569099 ) ) ;
#13088=CARTESIAN_POINT ( 'NONE',  ( -54.28335481156724285, 0.8699069336946697595, -4.241846523238430144 ) ) ;
#13119=AXIS2_PLACEMENT_3D ( 'NONE', #20303, #17905, #12990 ) ;
#13120=CARTESIAN_POINT ( 'NONE',  ( -57.72499999999997300, 0.9643027244899933237, -4.702139965541347166 ) ) ;
#13131=CARTESIAN_POINT ( 'NONE',  ( -56.54792740578360366, 3.330682475591790315, 0.6830477631804106053 ) ) ;
#13138=EDGE_CURVE ( 'NONE', #2190, #7150, #25440, .T. ) ;
#13157=CARTESIAN_POINT ( 'NONE',  ( -57.22499999999997300, 0.8236752438352034078, -4.016411220566566520 ) ) ;
#13167=ORIENTED_EDGE ( 'NONE', *, *, #11692, .F. ) ;
#13183=CARTESIAN_POINT ( 'NONE',  ( -56.90835481156724285, -0.7533615035077978472, 3.673546848079179750 ) ) ;
#13187=DIRECTION ( 'NONE',  ( 1.000000000000000000, 3.054025858079668409E-16, -2.042474015755241579E-16 ) ) ;
#13188=CARTESIAN_POINT ( 'NONE',  ( -55.62499999999997158, -3.673546848079173532, -0.7533615035078075062 ) ) ;
#13197=DIRECTION ( 'NONE',  ( 0.000000000000000000, 0.2008964009354148039, -0.9796124928211140670 ) ) ;
#13208=ORIENTED_EDGE ( 'NONE', *, *, #19964, .T. ) ;
#13226=ORIENTED_EDGE ( 'NONE', *, *, #22402, .F. ) ;
#13231=CARTESIAN_POINT ( 'NONE',  ( -54.59585481156724285, -2.489203624310586616, 2.804704140674918023 ) ) ;
#13234=ORIENTED_EDGE ( 'NONE', *, *, #18915, .T. ) ;
#13244=EDGE_CURVE ( 'NONE', #12772, #4965, #5957, .T. ) ;
#13253=ADVANCED_FACE ( 'NONE', ( #11520 ), #21352, .T. ) ;
#13271=CARTESIAN_POINT ( 'NONE',  ( -58.23542740578360366, 0.7887156198831662968, -3.845940847736174284 ) ) ;
#13286=CIRCLE ( 'NONE', #10772, 0.04999999999999988481 ) ;
#13287=AXIS2_PLACEMENT_3D ( 'NONE', #358, #14761, #19534 ) ;
#13297=ADVANCED_FACE ( 'NONE', ( #28607, #2159 ), #13712, .T. ) ;
#13305=ORIENTED_EDGE ( 'NONE', *, *, #6983, .F. ) ;
#13318=DIRECTION ( 'NONE',  ( 0.000000000000000000, -0.2008964009354148594, 0.9796124928211140670 ) ) ;
#13328=AXIS2_PLACEMENT_3D ( 'NONE', #13583, #11550, #21058 ) ;
#13355=CARTESIAN_POINT ( 'NONE',  ( -58.49999999999997158, -1.184343223768573594, -3.558065644182727638 ) ) ;
#13373=ADVANCED_FACE ( 'NONE', ( #15586 ), #27766, .F. ) ;
#13377=CARTESIAN_POINT ( 'NONE',  ( -57.34585481156722864, -1.184343223768586251, -3.558065644182725862 ) ) ;
#13385=DIRECTION ( 'NONE',  ( 1.000000000000000000, 3.054025858079668409E-16, -2.042474015755241579E-16 ) ) ;
#13401=CYLINDRICAL_SURFACE ( 'NONE', #10834, 3.750000000000000444 ) ;
#13408=CARTESIAN_POINT ( 'NONE',  ( -54.65835481156723574, -0.7533615035078032873, 3.673546848079177973 ) ) ;
#13410=CARTESIAN_POINT ( 'NONE',  ( -54.49999999999997868, -0.9643027244899872175, 4.702139965541346278 ) ) ;
#13421=CARTESIAN_POINT ( 'NONE',  ( -56.73542740578360366, 0.7887156198831665188, -3.845940847736174284 ) ) ;
#13438=EDGE_CURVE ( 'NONE', #13819, #11263, #21076, .T. ) ;
#13439=TOROIDAL_SURFACE ( 'NONE', #9925, 4.279289321881344144, 0.05000000000000000278 ) ;
#13479=AXIS2_PLACEMENT_3D ( 'NONE', #12999, #979, #351 ) ;
#13502=CARTESIAN_POINT ( 'NONE',  ( -59.29999999999994742, 2.202783890937385358, 2.955168114964210613 ) ) ;
#13505=EDGE_CURVE ( 'NONE', #5427, #23231, #20876, .T. ) ;
#13509=CIRCLE ( 'NONE', #17071, 3.750000000000000444 ) ;
#13528=DIRECTION ( 'NONE',  ( 1.000000000000000000, 3.054025858079668409E-16, -2.042474015755241579E-16 ) ) ;
#13541=DIRECTION ( 'NONE',  ( -1.000000000000000000, -3.054025858079668409E-16, 2.042474015755241579E-16 ) ) ;
#13546=ORIENTED_EDGE ( 'NONE', *, *, #20722, .F. ) ;
#13551=CARTESIAN_POINT ( 'NONE',  ( -56.15835481156723574, -0.8699069336946627651, 4.241846523238430144 ) ) ;
#13554=VERTEX_POINT ( 'NONE', #25993 ) ;
#13558=VERTEX_POINT ( 'NONE', #4299 ) ;
#13572=CARTESIAN_POINT ( 'NONE',  ( -58.98542740578360366, 0.7887156198831923870, -3.845940847736168511 ) ) ;
#13583=CARTESIAN_POINT ( 'NONE',  ( -59.29999999999997584, 2.330309927981284638E-15, 4.253626757584726372E-16 ) ) ;
#13587=CARTESIAN_POINT ( 'NONE',  ( -55.72085481156724285, 2.489203624310592833, -2.804704140674919799 ) ) ;
#13589=CARTESIAN_POINT ( 'NONE',  ( -58.54792740578360366, -2.256877952708263635, 2.542931754211924744 ) ) ;
#13591=PRODUCT_CONTEXT ( 'NONE', #7524, 'mechanical' ) ;
#13599=EDGE_CURVE ( 'NONE', #5317, #11953, #17107, .T. ) ;
#13608=CARTESIAN_POINT ( 'NONE',  ( -54.49999999999998579, 2.574607476582620347, -2.455998688455712120 ) ) ;
#13630=AXIS2_PLACEMENT_3D ( 'NONE', #30056, #30226, #24990 ) ;
#13635=ORIENTED_EDGE ( 'NONE', *, *, #9863, .T. ) ;
#13640=EDGE_CURVE ( 'NONE', #13558, #6742, #24102, .T. ) ;
#13652=EDGE_CURVE ( 'NONE', #6633, #11953, #4873, .T. ) ;
#13658=AXIS2_PLACEMENT_3D ( 'NONE', #1896, #9020, #16456 ) ;
#13701=CARTESIAN_POINT ( 'NONE',  ( -55.53335481156722864, 3.238593381231848145, 2.874284765127022467 ) ) ;
#13712=PLANE ( 'NONE',  #7983 ) ;
#13715=ORIENTED_EDGE ( 'NONE', *, *, #25014, .F. ) ;
#13722=CARTESIAN_POINT ( 'NONE',  ( -59.29895813073913047, -2.232665607824515952, 2.564420458051888563 ) ) ;
#13738=B_SPLINE_CURVE_WITH_KNOTS ( 'NONE', 3,
 ( #17754, #10148, #29306, #7621, #27394, #15207, #5232, #17900, #10617, #5705, #14739, #19815, #15354, #29447, #795, #25004, #3331, #12982 ),
 .UNSPECIFIED., .F., .F.,
 ( 4, 2, 2, 2, 2, 2, 2, 2, 4 ),
 ( 1.306736722590954369E-14, 0.0007570489093058673305, 0.001514097818598667423, 0.002271146727891467081, 0.003028195637184267174, 0.003785244546477067266, 0.004542293455769867358, 0.005299342365062667884, 0.006056391274355467542 ),
 .UNSPECIFIED. ) ;
#13743=CARTESIAN_POINT ( 'NONE',  ( -55.74999999999997158, -2.489203624310585283, 2.804704140674916690 ) ) ;
#13760=ORIENTED_EDGE ( 'NONE', *, *, #24314, .F. ) ;
#13767=EDGE_LOOP ( 'NONE', ( #11371, #22607, #13226, #27895 ) ) ;
#13813=DIRECTION ( 'NONE',  ( 1.000000000000000000, 3.054025858079668409E-16, -2.042474015755241579E-16 ) ) ;
#13818=ORIENTED_EDGE ( 'NONE', *, *, #4482, .T. ) ;
#13819=VERTEX_POINT ( 'NONE', #2372 ) ;
#13824=ORIENTED_EDGE ( 'NONE', *, *, #19889, .F. ) ;
#13826=CARTESIAN_POINT ( 'NONE',  ( -55.03335481156724995, 0.7533615035078067290, -3.673546848079180194 ) ) ;
#13835=DIRECTION ( 'NONE',  ( 1.000000000000000000, 3.054025858079668409E-16, -2.042474015755241579E-16 ) ) ;
#13845=CARTESIAN_POINT ( 'NONE',  ( -57.90835481156723574, 4.108500314926515351, -1.367561758111407899 ) ) ;
#13866=CARTESIAN_POINT ( 'NONE',  ( -56.47085481156723574, 2.489203624310592389, -2.804704140674919355 ) ) ;
#13869=CARTESIAN_POINT ( 'NONE',  ( -55.92292740578360366, 2.256877952708273405, -2.542931754211921636 ) ) ;
#13871=EDGE_CURVE ( 'NONE', #5904, #12772, #28654, .T. ) ;
#13891=LINE ( 'NONE', #28805, #12020 ) ;
#13895=CARTESIAN_POINT ( 'NONE',  ( -55.37499999999997868, 2.489203624310591056, -2.804704140674918023 ) ) ;
#13939=ORIENTED_EDGE ( 'NONE', *, *, #26246, .T. ) ;
#13940=CONICAL_SURFACE ( 'NONE', #8389, 4.299999999999998934, 0.7853981633974466137 ) ;
#13947=AXIS2_PLACEMENT_3D ( 'NONE', #7635, #24561, #4950 ) ;
#13953=ADVANCED_FACE ( 'NONE', ( #9156 ), #4394, .F. ) ;
#13967=CIRCLE ( 'NONE', #3881, 4.600000000000000533 ) ;
#13973=LINE ( 'NONE', #4321, #18451 ) ;
#13996=TOROIDAL_SURFACE ( 'NONE', #12481, 4.800000000000000711, 0.05000000000000000278 ) ;
#14006=DIRECTION ( 'NONE',  ( 0.000000000000000000, -0.2008964009354147484, 0.9796124928211140670 ) ) ;
#14016=CARTESIAN_POINT ( 'NONE',  ( -57.97085481156723574, 2.489203624310592389, -2.804704140674918911 ) ) ;
#14019=ORIENTED_EDGE ( 'NONE', *, *, #9701, .F. ) ;
#14029=ORIENTED_EDGE ( 'NONE', *, *, #12223, .T. ) ;
#14043=AXIS2_PLACEMENT_3D ( 'NONE', #29819, #15253, #13318 ) ;
#14046=CARTESIAN_POINT ( 'NONE',  ( -57.42292740578360366, 2.256877952708274737, -2.542931754211919859 ) ) ;
#14055=VERTEX_POINT ( 'NONE', #12286 ) ;
#14069=CARTESIAN_POINT ( 'NONE',  ( -56.99999999999997158, -1.184343223768585807, -3.558065644182723641 ) ) ;
#14126=LINE ( 'NONE', #14282, #26084 ) ;
#14133=DIRECTION ( 'NONE',  ( -1.000000000000000000, -3.054025858079668409E-16, 2.042474015755241579E-16 ) ) ;
#14136=ORIENTED_EDGE ( 'NONE', *, *, #18412, .T. ) ;
#14141=CARTESIAN_POINT ( 'NONE',  ( -55.99999999999997868, 3.673546848079180638, 0.7533615035078057298 ) ) ;
#14163=FACE_OUTER_BOUND ( 'NONE', #24327, .T. ) ;
#14174=CARTESIAN_POINT ( 'NONE',  ( -55.84599364905388086, 0.2309624077929090247, 3.875409454552789956 ) ) ;
#14181=CARTESIAN_POINT ( 'NONE',  ( -54.42292740578361077, 2.256877952708269852, -2.542931754211926076 ) ) ;
#14205=CARTESIAN_POINT ( 'NONE',  ( -58.54792740578360366, -2.256877952708278290, 2.542931754211911866 ) ) ;
#14217=ORIENTED_EDGE ( 'NONE', *, *, #24704, .F. ) ;
#14225=CARTESIAN_POINT ( 'NONE',  ( -61.04792740578359656, 3.330682475591789427, 0.6830477631804114935 ) ) ;
#14233=CARTESIAN_POINT ( 'NONE',  ( -59.22099364905385954, -0.2309624077928886521, -3.875409454552786848 ) ) ;
#14237=CYLINDRICAL_SURFACE ( 'NONE', #8928, 2.100000000000000089 ) ;
#14243=FACE_OUTER_BOUND ( 'NONE', #10367, .T. ) ;
#14252=EDGE_LOOP ( 'NONE', ( #10743, #28406, #23488, #14658, #2765, #8415, #123, #27454, #24511, #5370, #9697, #17223, #14729, #1839, #27683, #29431, #4527 ) ) ;
#14257=CARTESIAN_POINT ( 'NONE',  ( -59.22085481156723574, 1.184343223768590692, 3.558065644182727638 ) ) ;
#14267=CARTESIAN_POINT ( 'NONE',  ( -56.22099364905386665, -0.2309624077928977004, -3.875409454552789956 ) ) ;
#14269=ORIENTED_EDGE ( 'NONE', *, *, #23024, .F. ) ;
#14276=ORIENTED_EDGE ( 'NONE', *, *, #18558, .F. ) ;
#14280=CARTESIAN_POINT ( 'NONE',  ( -57.49999999999997158, 3.673546848079180194, 0.7533615035078097266 ) ) ;
#14282=CARTESIAN_POINT ( 'NONE',  ( -67.99999999999997158, -0.6177564328764010293, 3.012308415424927777 ) ) ;
#14290=EDGE_LOOP ( 'NONE', ( #23532, #26487, #18231, #19999 ) ) ;
#14330=ORIENTED_EDGE ( 'NONE', *, *, #19296, .F. ) ;
#14334=CARTESIAN_POINT ( 'NONE',  ( -54.92292740578361077, 1.073804522883522239, 3.225979517392335794 ) ) ;
#14339=DIRECTION ( 'NONE',  ( 1.000000000000000000, 3.054025858079668409E-16, -2.042474015755241579E-16 ) ) ;
#14353=CARTESIAN_POINT ( 'NONE',  ( -56.40835481156723574, 4.108500314926515351, -1.367561758111408565 ) ) ;
#14376=CARTESIAN_POINT ( 'NONE',  ( -54.81249999999997868, -3.238593381231840151, -2.874284765127021579 ) ) ;
#14378=DIRECTION ( 'NONE',  ( 0.000000000000000000, 0.2008964009354148594, -0.9796124928211140670 ) ) ;
#14398=LINE ( 'NONE', #9976, #4326 ) ;
#14411=CARTESIAN_POINT ( 'NONE',  ( -57.34585481156722864, -1.184343223768586251, -3.558065644182725862 ) ) ;
#14421=( BOUNDED_CURVE ( )  B_SPLINE_CURVE ( 2, ( #11057, #20735, #18348, #30362, #27986, #6300, #15950, #25611, #3932 ),
 .UNSPECIFIED., .F., .T. ) 
 B_SPLINE_CURVE_WITH_KNOTS ( ( 3, 2, 2, 2, 3 ),
 ( 0.3611111111111111049, 0.3703703703703703498, 0.3888888888888888951, 0.4074074074074073848, 0.4166666666666666852 ),
 .UNSPECIFIED. ) 
 CURVE ( )  GEOMETRIC_REPRESENTATION_ITEM ( )  RATIONAL_B_SPLINE_CURVE ( ( 0.9330127018922194093, 0.9330127018922194093, 1.000000000000000000, 0.8660254037844387076, 1.000000000000000000, 0.8660254037844387076, 1.000000000000000000, 0.9330127018922191873, 0.9330127018922194093 ) ) 
 REPRESENTATION_ITEM ( '' )  );
#14432=CARTESIAN_POINT ( 'NONE',  ( -58.03335481156722864, 0.7533615035077975142, -3.673546848079180638 ) ) ;
#14443=ORIENTED_EDGE ( 'NONE', *, *, #9759, .T. ) ;
#14466=CIRCLE ( 'NONE', #2332, 2.765000000000001013 ) ;
#14498=CARTESIAN_POINT ( 'NONE',  ( -54.79792740578361077, -2.256877952708263191, 2.542931754211923856 ) ) ;
#14501=EDGE_LOOP ( 'NONE', ( #8387, #25285, #15277, #5438 ) ) ;
#14531=DIRECTION ( 'NONE',  ( 0.000000000000000000, -1.000000000000000000, 0.000000000000000000 ) ) ;
#14542=EDGE_LOOP ( 'NONE', ( #96, #20320, #2082, #12618 ) ) ;
#14549=VECTOR ( 'NONE', #8201, 1000.000000000000000 ) ;
#14551=CARTESIAN_POINT ( 'NONE',  ( -57.06249999999997158, -3.238593381231840151, -2.874284765127021579 ) ) ;
#14570=DIRECTION ( 'NONE',  ( -1.000000000000000000, -3.054025858079668409E-16, 2.042474015755241579E-16 ) ) ;
#14584=CARTESIAN_POINT ( 'NONE',  ( -59.92928932188130631, 2.138123341857387114E-15, 5.538933845919563674E-16 ) ) ;
#14590=ADVANCED_FACE ( 'NONE', ( #23139 ), #30077, .F. ) ;
#14598=CARTESIAN_POINT ( 'NONE',  ( -57.22499999999997300, 2.964020293532818446E-15, 1.549317489258299684E-18 ) ) ;
#14599=CARTESIAN_POINT ( 'NONE',  ( -58.34585481156723574, -2.489203624310587060, 2.804704140674918911 ) ) ;
#14611=DIRECTION ( 'NONE',  ( -2.614375865348240525E-16, 0.2008964009354147207, -0.9796124928211138450 ) ) ;
#14616=DIRECTION ( 'NONE',  ( -1.000000000000000000, -3.054025858079668409E-16, 2.042474015755241579E-16 ) ) ;
#14634=DIRECTION ( 'NONE',  ( 2.581436205204234006E-16, -0.9796124928211140670, -0.2008964009354148872 ) ) ;
#14640=ADVANCED_FACE ( 'NONE', ( #10769 ), #18059, .T. ) ;
#14647=AXIS2_PLACEMENT_3D ( 'NONE', #6133, #6277, #3597 ) ;
#14655=CARTESIAN_POINT ( 'NONE',  ( -56.67292740578360366, 2.256877952708269408, -2.542931754211925188 ) ) ;
#14658=ORIENTED_EDGE ( 'NONE', *, *, #25014, .T. ) ;
#14664=ORIENTED_EDGE ( 'NONE', *, *, #4035, .T. ) ;
#14688=VERTEX_POINT ( 'NONE', #27873 ) ;
#14693=CARTESIAN_POINT ( 'NONE',  ( -67.98046642889043767, 0.6631150920522007608, -3.233486639521205852 ) ) ;
#14701=CARTESIAN_POINT ( 'NONE',  ( -60.87499999999996447, -3.673546848079174865, -0.7533615035078055078 ) ) ;
#14707=CARTESIAN_POINT ( 'NONE',  ( -54.49999999999997868, -0.2226148165844518412, -3.434203345966388543 ) ) ;
#14720=ADVANCED_FACE ( 'NONE', ( #14243 ), #21544, .F. ) ;
#14729=ORIENTED_EDGE ( 'NONE', *, *, #7003, .T. ) ;
#14734=CARTESIAN_POINT ( 'NONE',  ( -54.98542740578361077, 2.936324665650207333, 2.606018187048498191 ) ) ;
#14739=CARTESIAN_POINT ( 'NONE',  ( -59.29999999999994742, -3.524955859648372769, 0.4973042051317699275 ) ) ;
#14761=DIRECTION ( 'NONE',  ( 1.000000000000000000, 3.054025858079668409E-16, -2.042474015755241579E-16 ) ) ;
#14769=EDGE_LOOP ( 'NONE', ( #12244, #29237 ) ) ;
#14784=CARTESIAN_POINT ( 'NONE',  ( -56.72499999999997300, 3.116721586436802063E-15, -1.005743832985040150E-16 ) ) ;
#14797=AXIS2_PLACEMENT_3D ( 'NONE', #4018, #4167, #15885 ) ;
#14798=CARTESIAN_POINT ( 'NONE',  ( -56.11042740578360366, -2.936324665650200672, -2.606018187048498191 ) ) ;
#14841=CARTESIAN_POINT ( 'NONE',  ( -60.49999999999997158, 3.673546848079180194, 0.7533615035078067290 ) ) ;
#14843=LINE ( 'NONE', #12628, #14549 ) ;
#14848=CARTESIAN_POINT ( 'NONE',  ( -67.99999999999997158, 2.708628542650380666, 0.5554785485864246475 ) ) ;
#14869=ORIENTED_EDGE ( 'NONE', *, *, #13599, .F. ) ;
#14877=CARTESIAN_POINT ( 'NONE',  ( -55.42292740578360366, -3.330682475591783209, -0.6830477631804113825 ) ) ;
#14891=CARTESIAN_POINT ( 'NONE',  ( -71.44999999999998863, -1.380331489585512972E-15, 2.906968604901091669E-15 ) ) ;
#14939=ADVANCED_FACE ( 'NONE', ( #21870 ), #14952, .T. ) ;
#14946=ORIENTED_EDGE ( 'NONE', *, *, #29123, .F. ) ;
#14948=CARTESIAN_POINT ( 'NONE',  ( -60.42292740578359656, 2.256877952708268520, -2.542931754211924300 ) ) ;
#14952=TOROIDAL_SURFACE ( 'NONE', #31147, 4.800000000000000711, 0.05000000000000000278 ) ;
#14957=DIRECTION ( 'NONE',  ( 0.000000000000000000, -1.000000000000000000, 0.000000000000000000 ) ) ;
#14966=AXIS2_PLACEMENT_3D ( 'NONE', #16494, #18879, #25983 ) ;
#14995=ORIENTED_EDGE ( 'NONE', *, *, #18671, .F. ) ;
#15003=CARTESIAN_POINT ( 'NONE',  ( -60.12499999999996447, -3.673546848079174421, -0.7533615035078056188 ) ) ;
#15006=CARTESIAN_POINT ( 'NONE',  ( -58.03335481156722864, 0.7533615035077975142, -3.673546848079180638 ) ) ;
#15009=CARTESIAN_POINT ( 'NONE',  ( -54.49999999999998579, -3.534339970052580160, -1.064353278733559893 ) ) ;
#15025=CARTESIAN_POINT ( 'NONE',  ( -56.90400635094608361, 1.737685414808523454, -3.471684241605564658 ) ) ;
#15028=ORIENTED_EDGE ( 'NONE', *, *, #3756, .T. ) ;
#15038=EDGE_CURVE ( 'NONE', #5081, #19802, #25152, .T. ) ;
#15050=TOROIDAL_SURFACE ( 'NONE', #21666, 4.800000000000000711, 0.05000000000000000278 ) ;
#15054=ADVANCED_FACE ( 'NONE', ( #5169 ), #2790, .T. ) ;
#15117=CARTESIAN_POINT ( 'NONE',  ( -57.98542740578359656, 2.936324665650206889, 2.606018187048499080 ) ) ;
#15150=EDGE_CURVE ( 'NONE', #12762, #29802, #18505, .T. ) ;
#15168=CARTESIAN_POINT ( 'NONE',  ( -57.43749999999997868, 3.238593381231845481, 2.874284765127021579 ) ) ;
#15191=EDGE_CURVE ( 'NONE', #20706, #333, #7375, .T. ) ;
#15207=CARTESIAN_POINT ( 'NONE',  ( -59.29999999999996874, -3.436256089820699522, -1.251858815887733289 ) ) ;
#15209=ORIENTED_EDGE ( 'NONE', *, *, #10653, .F. ) ;
#15215=EDGE_CURVE ( 'NONE', #29380, #2983, #9420, .T. ) ;
#15230=DIRECTION ( 'NONE',  ( 1.000000000000000000, 3.054025858079668409E-16, -2.042474015755241579E-16 ) ) ;
#15243=( NAMED_UNIT ( * ) PLANE_ANGLE_UNIT ( ) SI_UNIT ( $, .RADIAN. ) );
#15253=DIRECTION ( 'NONE',  ( -2.581436205204234499E-16, 0.9796124928211140670, 0.2008964009354147762 ) ) ;
#15273=CARTESIAN_POINT ( 'NONE',  ( -58.86042740578360366, 3.725040285533370632, -1.239922660687675648 ) ) ;
#15277=ORIENTED_EDGE ( 'NONE', *, *, #10566, .T. ) ;
#15291=EDGE_CURVE ( 'NONE', #11104, #11593, #19522, .T. ) ;
#15301=CARTESIAN_POINT ( 'NONE',  ( -59.29999999999998295, -1.825148624098436478, 2.913569361162840377 ) ) ;
#15323=CARTESIAN_POINT ( 'NONE',  ( -54.49999999999997158, -3.743960284996337151, -0.06497723394329793511 ) ) ;
#15330=CARTESIAN_POINT ( 'NONE',  ( -55.36042740578360366, -2.936324665650197563, -2.606018187048502632 ) ) ;
#15336=ADVANCED_FACE ( 'NONE', ( #30805 ), #24106, .T. ) ;
#15338=VERTEX_POINT ( 'NONE', #26045 ) ;
#15344=ORIENTED_EDGE ( 'NONE', *, *, #16203, .F. ) ;
#15345=ORIENTED_EDGE ( 'NONE', *, *, #22754, .F. ) ;
#15354=CARTESIAN_POINT ( 'NONE',  ( -59.29999999999996163, -3.297590540183683139, 1.214612339250627171 ) ) ;
#15400=ADVANCED_FACE ( 'NONE', ( #87 ), #29140, .F. ) ;
#15415=CARTESIAN_POINT ( 'NONE',  ( -59.29999999999997584, 2.330309927981285032E-15, 4.253626757584724400E-16 ) ) ;
#15424=CARTESIAN_POINT ( 'NONE',  ( -58.54792740578360366, -2.256877952708263635, 2.542931754211924744 ) ) ;
#15440=AXIS2_PLACEMENT_3D ( 'NONE', #18300, #13528, #5347 ) ;
#15453=CARTESIAN_POINT ( 'NONE',  ( -58.53335481156722864, 3.238593381231847257, 2.874284765127023356 ) ) ;
#15476=FACE_OUTER_BOUND ( 'NONE', #18057, .T. ) ;
#15486=( NAMED_UNIT ( * ) SI_UNIT ( $, .STERADIAN. ) SOLID_ANGLE_UNIT ( ) );
#15495=DIRECTION ( 'NONE',  ( 2.614375865348240525E-16, -0.2008964009354147762, 0.9796124928211140670 ) ) ;
#15510=CARTESIAN_POINT ( 'NONE',  ( -58.06249999999996447, -0.7533615035078129463, 3.673546848079175309 ) ) ;
#15521=CARTESIAN_POINT ( 'NONE',  ( -60.54999999999995453, -0.7328781032566554776, 3.573665542649864246 ) ) ;
#15522=CARTESIAN_POINT ( 'NONE',  ( -59.23542740578359656, -3.725040285533365747, 1.239922660687675871 ) ) ;
#15526=( NAMED_UNIT ( * ) PLANE_ANGLE_UNIT ( ) SI_UNIT ( $, .RADIAN. ) );
#15562=DIRECTION ( 'NONE',  ( 0.000000000000000000, 0.2008964009354147762, -0.9796124928211140670 ) ) ;
#15566=CARTESIAN_POINT ( 'NONE',  ( -68.01382336603234080, 0.6601810586021495952, -3.219179684251513685 ) ) ;
#15577=CARTESIAN_POINT ( 'NONE',  ( -59.29999999999997584, 2.330309927981285032E-15, 4.253626757584724400E-16 ) ) ;
#15580=LINE ( 'NONE', #3545, #29704 ) ;
#15584=CARTESIAN_POINT ( 'NONE',  ( -54.49999999999997868, 3.673546848079182858, 0.7533615035078058408 ) ) ;
#15586=FACE_OUTER_BOUND ( 'NONE', #26800, .T. ) ;
#15597=CARTESIAN_POINT ( 'NONE',  ( -58.79792740578360366, 3.330682475591789427, 0.6830477631804110494 ) ) ;
#15611=EDGE_LOOP ( 'NONE', ( #25830, #25839, #6270, #27586 ) ) ;
#15613=PLANE ( 'NONE',  #27 ) ;
#15626=DIRECTION ( 'NONE',  ( 0.000000000000000000, -0.2008964009354147484, 0.9796124928211138450 ) ) ;
#15637=CARTESIAN_POINT ( 'NONE',  ( -54.84585481156724285, 3.673546848079182858, 0.7533615035078058408 ) ) ;
#15680=DIRECTION ( 'NONE',  ( 2.614375865348240525E-16, -0.2008964009354147762, 0.9796124928211140670 ) ) ;
#15682=CARTESIAN_POINT ( 'NONE',  ( -59.11042740578359656, -2.936324665650201560, -2.606018187048497747 ) ) ;
#15695=CARTESIAN_POINT ( 'NONE',  ( -59.29999999999997584, 2.330309927981285032E-15, 4.253626757584724400E-16 ) ) ;
#15724=ORIENTED_EDGE ( 'NONE', *, *, #23780, .F. ) ;
#15739=VERTEX_POINT ( 'NONE', #9711 ) ;
#15755=EDGE_LOOP ( 'NONE', ( #17548, #22297, #3210, #25574 ) ) ;
#15759=ORIENTED_EDGE ( 'NONE', *, *, #15038, .T. ) ;
#15760=CARTESIAN_POINT ( 'NONE',  ( -69.22071067811863543, 0.4319272620111411776, -2.106166859565393068 ) ) ;
#15783=CARTESIAN_POINT ( 'NONE',  ( -58.34585481156723574, -2.489203624310587060, 2.804704140674918911 ) ) ;
#15792=DIRECTION ( 'NONE',  ( 0.000000000000000000, 0.2008964009354147484, -0.9796124928211139560 ) ) ;
#15806=CARTESIAN_POINT ( 'NONE',  ( -54.86042740578361077, -0.7887156198831597465, 3.845940847736172952 ) ) ;
#15822=CARTESIAN_POINT ( 'NONE',  ( -57.29792740578360366, 3.330682475591789871, 0.6830477631804107164 ) ) ;
#15831=EDGE_CURVE ( 'NONE', #5422, #9091, #2722, .T. ) ;
#15848=ORIENTED_EDGE ( 'NONE', *, *, #11260, .T. ) ;
#15870=FACE_OUTER_BOUND ( 'NONE', #19767, .T. ) ;
#15873=CARTESIAN_POINT ( 'NONE',  ( -69.19999999999998863, -6.931756715175872842E-16, 2.447411951356162049E-15 ) ) ;
#15876=CARTESIAN_POINT ( 'NONE',  ( -55.56249999999997158, -3.238593381231837043, -2.874284765127025576 ) ) ;
#15884=AXIS2_PLACEMENT_3D ( 'NONE', #29565, #26580, #5346 ) ;
#15885=DIRECTION ( 'NONE',  ( 0.000000000000000000, 0.2008964009354147207, -0.9796124928211139560 ) ) ;
#15888=ORIENTED_EDGE ( 'NONE', *, *, #15215, .T. ) ;
#15897=AXIS2_PLACEMENT_3D ( 'NONE', #2766, #22113, #403 ) ;
#15900=ORIENTED_EDGE ( 'NONE', *, *, #21553, .T. ) ;
#15920=EDGE_LOOP ( 'NONE', ( #11317, #5647 ) ) ;
#15923=CARTESIAN_POINT ( 'NONE',  ( -56.34585481156723574, 3.673546848079182858, 0.7533615035078061739 ) ) ;
#15925=FACE_OUTER_BOUND ( 'NONE', #1703, .T. ) ;
#15931=CARTESIAN_POINT ( 'NONE',  ( -67.99999999999997158, -3.266925685480240183E-16, 2.202315069465531314E-15 ) ) ;
#15932=EDGE_LOOP ( 'NONE', ( #16138, #6726, #4706, #13824 ) ) ;
#15935=AXIS2_PLACEMENT_3D ( 'NONE', #3020, #8087, #484 ) ;
#15945=EDGE_CURVE ( 'NONE', #11521, #18051, #27145, .T. ) ;
#15949=CARTESIAN_POINT ( 'NONE',  ( -58.79792740578360366, 3.330682475591788982, 0.6830477631804159344 ) ) ;
#15950=CARTESIAN_POINT ( 'NONE',  ( -56.84585481156722864, -2.489203624310586616, 2.804704140674918467 ) ) ;
#15971=CARTESIAN_POINT ( 'NONE',  ( -56.67292740578360366, 2.256877952708269408, -2.542931754211925188 ) ) ;
#15974=DIRECTION ( 'NONE',  ( -2.614381936396368743E-16, 0.2008964009354147762, -0.9796124928211139560 ) ) ;
#16002=AXIS2_PLACEMENT_3D ( 'NONE', #16200, #6690, #7022 ) ;
#16025=AXIS2_PLACEMENT_3D ( 'NONE', #16, #12048, #17257 ) ;
#16038=FACE_OUTER_BOUND ( 'NONE', #11748, .T. ) ;
#16068=CARTESIAN_POINT ( 'NONE',  ( -69.22071067811863543, -6.995007661688606141E-16, 2.451642053546763754E-15 ) ) ;
#16084=DIRECTION ( 'NONE',  ( 1.000000000000000000, 3.054025858079668409E-16, -2.042474015755241579E-16 ) ) ;
#16091=EDGE_CURVE ( 'NONE', #8907, #24531, #23046, .T. ) ;
#16100=( BOUNDED_CURVE ( )  B_SPLINE_CURVE ( 2, ( #13183, #20194, #20496, #1157, #7988, #5924, #20021, #17807, #17651 ),
 .UNSPECIFIED., .F., .T. ) 
 B_SPLINE_CURVE_WITH_KNOTS ( ( 3, 2, 2, 2, 3 ),
 ( 0.4166666666666666852, 0.4259259259259259300, 0.4444444444444444198, 0.4629629629629629650, 0.4722222222222222099 ),
 .UNSPECIFIED. ) 
 CURVE ( )  GEOMETRIC_REPRESENTATION_ITEM ( )  RATIONAL_B_SPLINE_CURVE ( ( 0.9330127018922194093, 0.9330127018922195203, 1.000000000000000000, 0.8660254037844387076, 1.000000000000000000, 0.8660254037844387076, 1.000000000000000000, 0.9330127018922194093, 0.9330127018922194093 ) ) 
 REPRESENTATION_ITEM ( '' )  );
#16103=CARTESIAN_POINT ( 'NONE',  ( -58.90835481156722864, -3.238593381231842816, -2.874284765127022023 ) ) ;
#16112=DIRECTION ( 'NONE',  ( 0.000000000000000000, 0.2008964009354147762, -0.9796124928211140670 ) ) ;
#16113=CARTESIAN_POINT ( 'NONE',  ( -71.49999999999998579, -1.395601618875910821E-15, 2.917180974979867506E-15 ) ) ;
#16125=CARTESIAN_POINT ( 'NONE',  ( -59.17292740578360366, -3.330682475591780101, -0.6830477631804271477 ) ) ;
#16138=ORIENTED_EDGE ( 'NONE', *, *, #16340, .T. ) ;
#16146=CARTESIAN_POINT ( 'NONE',  ( -58.04792740578360366, 3.330682475591789427, 0.6830477631804109384 ) ) ;
#16200=CARTESIAN_POINT ( 'NONE',  ( -57.22499999999997300, 2.964020293532818446E-15, 1.549317489258312010E-18 ) ) ;
#16203=EDGE_CURVE ( 'NONE', #28519, #7502, #16718, .T. ) ;
#16225=CARTESIAN_POINT ( 'NONE',  ( -61.06249999999995737, -0.8699069336946632092, 4.241846523238429256 ) ) ;
#16233=DIRECTION ( 'NONE',  ( 0.000000000000000000, -0.2008964009354152203, 0.9796124928211138450 ) ) ;
#16239=FACE_OUTER_BOUND ( 'NONE', #17723, .T. ) ;
#16247=CARTESIAN_POINT ( 'NONE',  ( -67.99999999999997158, 0.3264566515200485464, -1.591870300834308471 ) ) ;
#16255=CARTESIAN_POINT ( 'NONE',  ( -58.72085481156723574, 2.489203624310592389, -2.804704140674918911 ) ) ;
#16265=CARTESIAN_POINT ( 'NONE',  ( -60.44999999999996021, -0.8596938233273121455, 4.192045280110958672 ) ) ;
#16280=CARTESIAN_POINT ( 'NONE',  ( -55.67292740578360366, 1.073804522883521573, 3.225979517392336238 ) ) ;
#16304=CARTESIAN_POINT ( 'NONE',  ( -59.73542740578360366, 0.7887156198831659637, -3.845940847736173840 ) ) ;
#16309=DIRECTION ( 'NONE',  ( 0.000000000000000000, 0.2008964009354147484, -0.9796124928211139560 ) ) ;
#16311=EDGE_LOOP ( 'NONE', ( #8973, #4967, #25399, #3408 ) ) ;
#16340=EDGE_CURVE ( 'NONE', #11624, #16493, #18502, .T. ) ;
#16353=CARTESIAN_POINT ( 'NONE',  ( -58.02900635094607651, -1.737685414808523232, 3.471684241605558885 ) ) ;
#16361=CARTESIAN_POINT ( 'NONE',  ( -69.22071067811863543, -6.995007661688606141E-16, 2.451642053546763754E-15 ) ) ;
#16395=DIRECTION ( 'NONE',  ( 1.000000000000000000, 3.054025858079668409E-16, -2.042474015755241579E-16 ) ) ;
#16405=CARTESIAN_POINT ( 'NONE',  ( -58.15835481156722864, -3.238593381231841928, -2.874284765127022023 ) ) ;
#16425=( BOUNDED_CURVE ( )  B_SPLINE_CURVE ( 2, ( #6109, #25409, #13355, #28893, #26357, #21320, #31097, #30950, #26680 ),
 .UNSPECIFIED., .F., .T. ) 
 B_SPLINE_CURVE_WITH_KNOTS ( ( 3, 2, 2, 2, 3 ),
 ( 0.5833333333333333703, 0.5925925925925925597, 0.6111111111111111605, 0.6296296296296296502, 0.6388888888888889506 ),
 .UNSPECIFIED. ) 
 CURVE ( )  GEOMETRIC_REPRESENTATION_ITEM ( )  RATIONAL_B_SPLINE_CURVE ( ( 0.9330127018922194093, 0.9330127018922197424, 1.000000000000000000, 0.8660254037844387076, 1.000000000000000000, 0.8660254037844387076, 1.000000000000000000, 0.9330127018922189652, 0.9330127018922194093 ) ) 
 REPRESENTATION_ITEM ( '' )  );
#16428=CARTESIAN_POINT ( 'NONE',  ( -56.61042740578359656, 3.725040285533373741, -1.239922660687670986 ) ) ;
#16430=AXIS2_PLACEMENT_3D ( 'NONE', #8920, #6561, #25870 ) ;
#16451=CARTESIAN_POINT ( 'NONE',  ( -56.81249999999997868, 4.108500314926513575, -1.367561758111407455 ) ) ;
#16453=CIRCLE ( 'NONE', #2789, 3.286176633967618166 ) ;
#16456=DIRECTION ( 'NONE',  ( 0.000000000000000000, -0.2008964009354147484, 0.9796124928211139560 ) ) ;
#16478=EDGE_CURVE ( 'NONE', #26980, #709, #11010, .T. ) ;
#16491=CARTESIAN_POINT ( 'NONE',  ( -56.52900635094607651, -1.737685414808518347, 3.471684241605561994 ) ) ;
#16493=VERTEX_POINT ( 'NONE', #26207 ) ;
#16494=CARTESIAN_POINT ( 'NONE',  ( -56.67499999999996874, 3.131991715727200307E-15, -1.107867533772800737E-16 ) ) ;
#16513=AXIS2_PLACEMENT_3D ( 'NONE', #29631, #22068, #12691 ) ;
#16522=VECTOR ( 'NONE', #9906, 1000.000000000000114 ) ;
#16529=CARTESIAN_POINT ( 'NONE',  ( -71.49999999999998579, 0.4118376219175989839, -2.008205610283281040 ) ) ;
#16540=EDGE_LOOP ( 'NONE', ( #25660, #4364, #6364, #2630 ) ) ;
#16547=CIRCLE ( 'NONE', #6937, 4.800000000000000711 ) ;
#16558=CARTESIAN_POINT ( 'NONE',  ( -58.03335481156722864, 0.7533615035077975142, -3.673546848079180638 ) ) ;
#16560=CIRCLE ( 'NONE', #11990, 1.474464970144730991 ) ;
#16567=CARTESIAN_POINT ( 'NONE',  ( -67.97846802697301882, -0.6530782982312804963, 3.184545152421074388 ) ) ;
#16579=CARTESIAN_POINT ( 'NONE',  ( -59.78335481156722864, -4.108500314926510022, 1.367561758111408121 ) ) ;
#16605=CARTESIAN_POINT ( 'NONE',  ( -56.23542740578359656, -3.725040285533366191, 1.239922660687671652 ) ) ;
#16619=CARTESIAN_POINT ( 'NONE',  ( -71.44781903063172024, -1.379665415900875831E-15, 2.906523147574707464E-15 ) ) ;
#16628=CARTESIAN_POINT ( 'NONE',  ( -59.86042740578359656, -2.936324665650201116, -2.606018187048497303 ) ) ;
#16630=DIRECTION ( 'NONE',  ( 0.000000000000000000, -0.2008964009354147762, 0.9796124928211139560 ) ) ;
#16632=DIRECTION ( 'NONE',  ( -1.000000000000000000, -3.054027077731387480E-16, 2.042479963029832083E-16 ) ) ;
#16637=( BOUNDED_CURVE ( )  B_SPLINE_CURVE ( 2, ( #14432, #11909, #44, #31235, #9562, #1944, #14599, #21287, #9707 ),
 .UNSPECIFIED., .F., .T. ) 
 B_SPLINE_CURVE_WITH_KNOTS ( ( 3, 2, 2, 2, 3 ),
 ( 0.5833333333333333703, 0.5925925925925925597, 0.6111111111111111605, 0.6296296296296296502, 0.6388888888888889506 ),
 .UNSPECIFIED. ) 
 CURVE ( )  GEOMETRIC_REPRESENTATION_ITEM ( )  RATIONAL_B_SPLINE_CURVE ( ( 0.9330127018922194093, 0.9330127018922197424, 1.000000000000000000, 0.8660254037844387076, 1.000000000000000000, 0.8660254037844387076, 1.000000000000000000, 0.9330127018922189652, 0.9330127018922194093 ) ) 
 REPRESENTATION_ITEM ( '' )  );
#16642=CARTESIAN_POINT ( 'NONE',  ( -56.97099364905386665, -0.2309624077928983110, -3.875409454552788624 ) ) ;
#16685=CARTESIAN_POINT ( 'NONE',  ( -57.87499999999997158, -3.673546848079170424, -0.7533615035078229383 ) ) ;
#16689=EDGE_CURVE ( 'NONE', #31001, #3318, #1802, .T. ) ;
#16690=ORIENTED_EDGE ( 'NONE', *, *, #25578, .T. ) ;
#16691=DIRECTION ( 'NONE',  ( -1.000000000000000000, -3.054025858079668409E-16, 2.042474015755241579E-16 ) ) ;
#16703=ORIENTED_EDGE ( 'NONE', *, *, #23282, .F. ) ;
#16718=LINE ( 'NONE', #21467, #9889 ) ;
#16736=CARTESIAN_POINT ( 'NONE',  ( -54.67292740578360366, -3.330682475591782765, -0.6830477631804114935 ) ) ;
#16741=DIRECTION ( 'NONE',  ( -1.000000000000000000, -3.054025858079668409E-16, 2.042474015755241579E-16 ) ) ;
#16768=ORIENTED_EDGE ( 'NONE', *, *, #6255, .T. ) ;
#16779=CARTESIAN_POINT ( 'NONE',  ( -54.74999999999997868, -1.184343223768585140, -3.558065644182724085 ) ) ;
#16789=EDGE_CURVE ( 'NONE', #5317, #5591, #26829, .T. ) ;
#16804=VERTEX_POINT ( 'NONE', #24151 ) ;
#16835=CARTESIAN_POINT ( 'NONE',  ( -54.54999999999998295, -0.9643027244899872175, 4.702139965541346278 ) ) ;
#16846=CARTESIAN_POINT ( 'NONE',  ( -60.44999999999996021, 1.979096954302128589E-15, 6.602471875703214707E-16 ) ) ;
#16875=DIRECTION ( 'NONE',  ( -2.581436205204234499E-16, 0.9796124928211140670, 0.2008964009354147762 ) ) ;
#16885=CARTESIAN_POINT ( 'NONE',  ( -60.03335481156722864, 3.238593381231847257, 2.874284765127023356 ) ) ;
#16887=LINE ( 'NONE', #241, #16522 ) ;
#16902=CARTESIAN_POINT ( 'NONE',  ( -59.29999999999997584, -2.208048483361063852, 2.585444235547710967 ) ) ;
#16906=DIRECTION ( 'NONE',  ( 0.000000000000000000, 0.2008964009354147762, -0.9796124928211140670 ) ) ;
#16913=ORIENTED_EDGE ( 'NONE', *, *, #30042, .T. ) ;
#16928=CARTESIAN_POINT ( 'NONE',  ( -60.86042740578358945, -0.7887156198831608567, 3.845940847736174728 ) ) ;
#16933=ADVANCED_FACE ( 'NONE', ( #15870 ), #29144, .F. ) ;
#16935=( BOUNDED_SURFACE ( )  B_SPLINE_SURFACE ( 1, 2, ( 
 ( #22445, #22916, #3452, #13088, #29548, #22774, #18009, #27658, #13231, #5655, #5986, #5502, #15637, #1205, #587, #10246, #741, #10402, #20083, #29722, #8034, #17701, #11663, #13701, #3734, #23383, #30817, #1834, #11507, #28285, #9134, #18798, #6744, #13551, #6131, #27962, #15923, #4207, #26057, #3902, #11325, #21187, #11183, #6597, #6442, #23233, #28441, #1522, #21011, #4367, #30184, #8499, #13377, #28119, #27822, #8961, #23707, #20857, #8645, #30485, #25902, #13845, #14016, #1666, #1997, #16405, #18180, #8788, #15783, #25432, #23073, #30649, #6276, #18641, #16255, #23534, #1369, #16103, #11035, #20710, #30340, #18325, #25584, #18480, #25751, #4058, #28763, #7221, #7073, #2767, #19274, #16579, #24168, #26526, #2305, #16885, #21809, #30970, #19418, #4834, #9904, #6914, #28910, #2477, #5148, #29223, #12270, #26702, #21487 ),
 ( #21954, #7538, #14181, #2626, #24318, #18951, #16736, #28597, #14498, #239, #14334, #9755, #26378, #31120, #9453, #12131, #26224, #9288, #4530, #21341, #9616, #19585, #24004, #17198, #98, #4679, #4997, #11972, #26842, #14798, #29063, #23856, #2149, #24458, #7371, #21659, #11812, #19118, #14655, #31287, #17052, #17498, #24919, #3412, #24775, #10534, #20037, #5467, #1031, #27153, #3238, #8298, #12417, #22114, #26985, #10360, #10064, #22568, #5943, #15117, #22266, #3084, #8150, #27457, #27615, #27310, #17966, #22735, #15424, #12732, #10680, #13052, #15597, #15273, #10209, #12880, #875, #20208, #25243, #29681, #17821, #29838, #5291, #5623, #20364, #5772, #25076, #29987, #19878, #8000, #29508, #404, #17663, #7679, #19738, #29367, #22409, #17339, #14948, #24618, #2935, #12579, #552, #7822, #700, #6396, #18760, #11461, #25865 ) ),
 .UNSPECIFIED., .F., .F., .F. ) 
 B_SPLINE_SURFACE_WITH_KNOTS ( ( 2, 2 ),
 ( 3, 2, 2, 2, 2, 2, 2, 2, 2, 2, 2, 2, 2, 2, 2, 2, 2, 2, 2, 2, 2, 2, 2, 2, 2, 2, 2, 2, 2, 2, 2, 2, 2, 2, 2, 2, 2, 2, 2, 2, 2, 2, 2, 2, 2, 2, 2, 2, 2, 2, 2, 2, 2, 2, 3 ),
 ( 0.000000000000000000, 1.000000000000000000 ),
 ( 0.000000000000000000, 0.01851851851851851749, 0.03703703703703703498, 0.05555555555555555247, 0.07407407407407406996, 0.09259259259259258745, 0.1111111111111111049, 0.1296296296296296224, 0.1481481481481481399, 0.1666666666666666574, 0.1851851851851851749, 0.2037037037037036924, 0.2222222222222222099, 0.2407407407407407274, 0.2592592592592592449, 0.2777777777777777901, 0.2962962962962962798, 0.3148148148148148251, 0.3333333333333333148, 0.3518518518518518601, 0.3703703703703703498, 0.3888888888888888951, 0.4074074074074073848, 0.4259259259259259300, 0.4444444444444444198, 0.4629629629629629650, 0.4814814814814814548, 0.5000000000000000000, 0.5185185185185184897, 0.5370370370370370905, 0.5555555555555555802, 0.5740740740740740700, 0.5925925925925925597, 0.6111111111111111605, 0.6296296296296296502, 0.6481481481481481399, 0.6666666666666666297, 0.6851851851851852304, 0.7037037037037037202, 0.7222222222222222099, 0.7407407407407406996, 0.7592592592592593004, 0.7777777777777777901, 0.7962962962962962798, 0.8148148148148147696, 0.8333333333333333703, 0.8518518518518518601, 0.8703703703703703498, 0.8888888888888888395, 0.9074074074074074403, 0.9259259259259259300, 0.9444444444444444198, 0.9629629629629629095, 0.9814814814814815103, 1.000000000000000000 ),
 .UNSPECIFIED. ) 
 GEOMETRIC_REPRESENTATION_ITEM ( )  RATIONAL_B_SPLINE_SURFACE ( (
 ( 1.000000000000000000, 0.8660254037844387076, 1.000000000000000000, 0.8660254037844387076, 1.000000000000000000, 0.8660254037844387076, 1.000000000000000000, 0.8660254037844387076, 1.000000000000000000, 0.8660254037844387076, 1.000000000000000000, 0.8660254037844387076, 1.000000000000000000, 0.8660254037844387076, 1.000000000000000000, 0.8660254037844387076, 1.000000000000000000, 0.8660254037844387076, 1.000000000000000000, 0.8660254037844387076, 1.000000000000000000, 0.8660254037844387076, 1.000000000000000000, 0.8660254037844387076, 1.000000000000000000, 0.8660254037844387076, 1.000000000000000000, 0.8660254037844387076, 1.000000000000000000, 0.8660254037844387076, 1.000000000000000000, 0.8660254037844387076, 1.000000000000000000, 0.8660254037844387076, 1.000000000000000000, 0.8660254037844387076, 1.000000000000000000, 0.8660254037844387076, 1.000000000000000000, 0.8660254037844387076, 1.000000000000000000, 0.8660254037844387076, 1.000000000000000000, 0.8660254037844387076, 1.000000000000000000, 0.8660254037844387076, 1.000000000000000000, 0.8660254037844387076, 1.000000000000000000, 0.8660254037844387076, 1.000000000000000000, 0.8660254037844387076, 1.000000000000000000, 0.8660254037844387076, 1.000000000000000000, 0.8660254037844387076, 1.000000000000000000, 0.8660254037844387076, 1.000000000000000000, 0.8660254037844387076, 1.000000000000000000, 0.8660254037844387076, 1.000000000000000000, 0.8660254037844387076, 1.000000000000000000, 0.8660254037844387076, 1.000000000000000000, 0.8660254037844387076, 1.000000000000000000, 0.8660254037844387076, 1.000000000000000000, 0.8660254037844387076, 1.000000000000000000, 0.8660254037844387076, 1.000000000000000000, 0.8660254037844387076, 1.000000000000000000, 0.8660254037844387076, 1.000000000000000000, 0.8660254037844387076, 1.000000000000000000, 0.8660254037844387076, 1.000000000000000000, 0.8660254037844387076, 1.000000000000000000, 0.8660254037844387076, 1.000000000000000000, 0.8660254037844387076, 1.000000000000000000, 0.8660254037844387076, 1.000000000000000000, 0.8660254037844387076, 1.000000000000000000, 0.8660254037844387076, 1.000000000000000000, 0.8660254037844387076, 1.000000000000000000, 0.8660254037844387076, 1.000000000000000000, 0.8660254037844387076, 1.000000000000000000, 0.8660254037844387076, 1.000000000000000000, 0.8660254037844387076, 1.000000000000000000, 0.8660254037844387076, 1.000000000000000000, 0.8660254037844387076, 1.000000000000000000),
 ( 1.000000000000000000, 0.8660254037844387076, 1.000000000000000000, 0.8660254037844387076, 1.000000000000000000, 0.8660254037844387076, 1.000000000000000000, 0.8660254037844387076, 1.000000000000000000, 0.8660254037844387076, 1.000000000000000000, 0.8660254037844387076, 1.000000000000000000, 0.8660254037844387076, 1.000000000000000000, 0.8660254037844387076, 1.000000000000000000, 0.8660254037844387076, 1.000000000000000000, 0.8660254037844387076, 1.000000000000000000, 0.8660254037844387076, 1.000000000000000000, 0.8660254037844387076, 1.000000000000000000, 0.8660254037844387076, 1.000000000000000000, 0.8660254037844387076, 1.000000000000000000, 0.8660254037844387076, 1.000000000000000000, 0.8660254037844387076, 1.000000000000000000, 0.8660254037844387076, 1.000000000000000000, 0.8660254037844387076, 1.000000000000000000, 0.8660254037844387076, 1.000000000000000000, 0.8660254037844387076, 1.000000000000000000, 0.8660254037844387076, 1.000000000000000000, 0.8660254037844387076, 1.000000000000000000, 0.8660254037844387076, 1.000000000000000000, 0.8660254037844387076, 1.000000000000000000, 0.8660254037844387076, 1.000000000000000000, 0.8660254037844387076, 1.000000000000000000, 0.8660254037844387076, 1.000000000000000000, 0.8660254037844387076, 1.000000000000000000, 0.8660254037844387076, 1.000000000000000000, 0.8660254037844387076, 1.000000000000000000, 0.8660254037844387076, 1.000000000000000000, 0.8660254037844387076, 1.000000000000000000, 0.8660254037844387076, 1.000000000000000000, 0.8660254037844387076, 1.000000000000000000, 0.8660254037844387076, 1.000000000000000000, 0.8660254037844387076, 1.000000000000000000, 0.8660254037844387076, 1.000000000000000000, 0.8660254037844387076, 1.000000000000000000, 0.8660254037844387076, 1.000000000000000000, 0.8660254037844387076, 1.000000000000000000, 0.8660254037844387076, 1.000000000000000000, 0.8660254037844387076, 1.000000000000000000, 0.8660254037844387076, 1.000000000000000000, 0.8660254037844387076, 1.000000000000000000, 0.8660254037844387076, 1.000000000000000000, 0.8660254037844387076, 1.000000000000000000, 0.8660254037844387076, 1.000000000000000000, 0.8660254037844387076, 1.000000000000000000, 0.8660254037844387076, 1.000000000000000000, 0.8660254037844387076, 1.000000000000000000, 0.8660254037844387076, 1.000000000000000000, 0.8660254037844387076, 1.000000000000000000, 0.8660254037844387076, 1.000000000000000000, 0.8660254037844387076, 1.000000000000000000) ) ) 
 REPRESENTATION_ITEM ( '' )  SURFACE ( )  );
#16969=CARTESIAN_POINT ( 'NONE',  ( -56.37499999999997158, -3.673546848079171756, -0.7533615035078148336 ) ) ;
#16985=VECTOR ( 'NONE', #18040, 1000.000000000000000 ) ;
#17008=DIRECTION ( 'NONE',  ( 0.000000000000000000, 0.2008964009354147484, -0.9796124928211138450 ) ) ;
#17045=VECTOR ( 'NONE', #29938, 1000.000000000000000 ) ;
#17052=CARTESIAN_POINT ( 'NONE',  ( -56.79792740578360366, -1.073804522883517132, -3.225979517392335794 ) ) ;
#17062=ORIENTED_EDGE ( 'NONE', *, *, #11260, .F. ) ;
#17064=CARTESIAN_POINT ( 'NONE',  ( -57.22499999999997300, 2.964020293532818446E-15, 1.549317489258312010E-18 ) ) ;
#17069=EDGE_CURVE ( 'NONE', #29879, #24689, #14126, .T. ) ;
#17071=AXIS2_PLACEMENT_3D ( 'NONE', #31236, #4775, #12082 ) ;
#17092=ORIENTED_EDGE ( 'NONE', *, *, #21542, .T. ) ;
#17094=AXIS2_PLACEMENT_3D ( 'NONE', #15931, #3911, #11188 ) ;
#17100=CARTESIAN_POINT ( 'NONE',  ( -60.62499999999997158, 2.489203624310590168, -2.804704140674917134 ) ) ;
#17104=CARTESIAN_POINT ( 'NONE',  ( -54.49999999999999289, -1.466116979365514217, -3.192719761242667431 ) ) ;
#17106=CARTESIAN_POINT ( 'NONE',  ( -71.49999999999998579, -1.395601618875910821E-15, 2.917180974979867506E-15 ) ) ;
#17107=CIRCLE ( 'NONE', #5899, 3.300781342844381072 ) ;
#17134=CARTESIAN_POINT ( 'NONE',  ( -54.61042740578360366, -2.936324665650200672, -2.606018187048499080 ) ) ;
#17143=DIRECTION ( 'NONE',  ( 0.000000000000000000, 0.2008964009354141933, -0.9796124928211140670 ) ) ;
#17147=CIRCLE ( 'NONE', #19679, 0.04999999999999989175 ) ;
#17179=EDGE_CURVE ( 'NONE', #16493, #11263, #25571, .T. ) ;
#17190=PLANE ( 'NONE',  #6901 ) ;
#17198=CARTESIAN_POINT ( 'NONE',  ( -55.73542740578360366, 2.936324665650206889, 2.606018187048498191 ) ) ;
#17199=DIRECTION ( 'NONE',  ( 1.000000000000000000, 3.054025858079668409E-16, -2.042474015755241579E-16 ) ) ;
#17204=CARTESIAN_POINT ( 'NONE',  ( -55.97085481156723574, -3.673546848079175309, -0.7533615035078069511 ) ) ;
#17212=CYLINDRICAL_SURFACE ( 'NONE', #10726, 3.750000000000000444 ) ;
#17223=ORIENTED_EDGE ( 'NONE', *, *, #18029, .T. ) ;
#17228=CYLINDRICAL_SURFACE ( 'NONE', #30006, 3.750000000000000444 ) ;
#17232=CARTESIAN_POINT ( 'NONE',  ( -59.29999999999997584, -0.6177564328763985868, 3.012308415424926444 ) ) ;
#17244=CARTESIAN_POINT ( 'NONE',  ( -59.24999999999997158, -1.184343223768586029, -3.558065644182723197 ) ) ;
#17250=VERTEX_POINT ( 'NONE', #2416 ) ;
#17257=DIRECTION ( 'NONE',  ( -2.614375865348240525E-16, 0.2008964009354147762, -0.9796124928211140670 ) ) ;
#17275=CARTESIAN_POINT ( 'NONE',  ( -55.29792740578360366, -1.073804522883516688, -3.225979517392336238 ) ) ;
#17339=CARTESIAN_POINT ( 'NONE',  ( -60.36042740578359656, 3.725040285533370632, -1.239922660687674982 ) ) ;
#17347=CARTESIAN_POINT ( 'NONE',  ( -71.44999999999998863, 0.4218824419643697476, -2.057186234924337054 ) ) ;
#17350=CARTESIAN_POINT ( 'NONE',  ( -58.40400635094607651, 1.737685414808531892, -3.471684241605561549 ) ) ;
#17364=CARTESIAN_POINT ( 'NONE',  ( -59.29999999999998295, -2.024706599330198031, 2.760581573505366926 ) ) ;
#17370=EDGE_CURVE ( 'NONE', #14055, #26583, #23291, .T. ) ;
#17379=ORIENTED_EDGE ( 'NONE', *, *, #16091, .T. ) ;
#17383=CARTESIAN_POINT ( 'NONE',  ( -58.49999999999997158, -1.184343223768586029, -3.558065644182723641 ) ) ;
#17407=EDGE_LOOP ( 'NONE', ( #3367, #19992, #14869, #22699 ) ) ;
#17423=EDGE_LOOP ( 'NONE', ( #28242, #20761, #23713, #8724 ) ) ;
#17431=DIRECTION ( 'NONE',  ( 1.000000000000000000, 3.054025858079668409E-16, -2.042474015755241579E-16 ) ) ;
#17448=AXIS2_PLACEMENT_3D ( 'NONE', #5902, #27744, #30414 ) ;
#17498=CARTESIAN_POINT ( 'NONE',  ( -56.86042740578360366, -2.936324665650200672, -2.606018187048497747 ) ) ;
#17505=AXIS2_PLACEMENT_3D ( 'NONE', #14784, #7207, #26684 ) ;
#17510=CIRCLE ( 'NONE', #16513, 0.04999999999999987094 ) ;
#17539=ORIENTED_EDGE ( 'NONE', *, *, #1261, .T. ) ;
#17548=ORIENTED_EDGE ( 'NONE', *, *, #25846, .F. ) ;
#17552=CARTESIAN_POINT ( 'NONE',  ( -58.06249999999997158, -0.8699069336946626541, 4.241846523238428368 ) ) ;
#17572=DIRECTION ( 'NONE',  ( 0.000000000000000000, 0.2008964009354147762, -0.9796124928211140670 ) ) ;
#17574=DIRECTION ( 'NONE',  ( 0.000000000000000000, -0.2008964009354147762, 0.9796124928211139560 ) ) ;
#17576=EDGE_LOOP ( 'NONE', ( #17062, #16690, #9411, #6707 ) ) ;
#17586=CARTESIAN_POINT ( 'NONE',  ( -60.44999999999996021, 0.8596938233273155872, -4.192045280110956895 ) ) ;
#17591=CARTESIAN_POINT ( 'NONE',  ( -54.29792740578361077, 3.330682475591790315, 0.6830477631804100502 ) ) ;
#17616=DIRECTION ( 'NONE',  ( -1.000000000000000000, -3.054025858079668409E-16, 2.042474015755241579E-16 ) ) ;
#17651=CARTESIAN_POINT ( 'NONE',  ( -57.28335481156723574, 0.7533615035078095046, -3.673546848079178861 ) ) ;
#17662=CARTESIAN_POINT ( 'NONE',  ( -71.44999999999998863, -1.380331489585512972E-15, 2.906968604901091669E-15 ) ) ;
#17663=CARTESIAN_POINT ( 'NONE',  ( -60.04792740578359656, -2.256877952708263635, 2.542931754211925188 ) ) ;
#17668=CARTESIAN_POINT ( 'NONE',  ( -56.15835481156722153, -0.7533615035077977362, 3.673546848079179750 ) ) ;
#17701=CARTESIAN_POINT ( 'NONE',  ( -55.40835481156723574, -0.8699069336946626541, 4.241846523238430144 ) ) ;
#17706=PRODUCT_DEFINITION_FORMATION_WITH_SPECIFIED_SOURCE ( 'ANY', '', #20207, .NOT_KNOWN. ) ;
#17723=EDGE_LOOP ( 'NONE', ( #21298, #10860, #22705, #26270 ) ) ;
#17728=DIRECTION ( 'NONE',  ( -1.000000000000000000, -3.054025858079668409E-16, 2.042474015755241579E-16 ) ) ;
#17737=PRODUCT_DEFINITION_CONTEXT ( 'detailed design', #31246, 'design' ) ;
#17754=CARTESIAN_POINT ( 'NONE',  ( -59.30000000000042348, -2.541725022351402963, -2.757196748647571027 ) ) ;
#17784=ORIENTED_EDGE ( 'NONE', *, *, #26278, .T. ) ;
#17807=CARTESIAN_POINT ( 'NONE',  ( -57.24986116251334778, 1.737685414808521678, -3.471684241605565546 ) ) ;
#17821=CARTESIAN_POINT ( 'NONE',  ( -59.29792740578359656, -2.256877952708263635, 2.542931754211925188 ) ) ;
#17843=CARTESIAN_POINT ( 'NONE',  ( -58.78335481156722864, 0.7533615035077975142, -3.673546848079180638 ) ) ;
#17859=DIRECTION ( 'NONE',  ( 2.581436205204234006E-16, -0.9796124928211140670, -0.2008964009354148872 ) ) ;
#17870=( LENGTH_UNIT ( ) NAMED_UNIT ( * ) SI_UNIT ( .MILLI., .METRE. ) );
#17876=CARTESIAN_POINT ( 'NONE',  ( -54.54792740578361077, -1.073804522883516688, -3.225979517392336238 ) ) ;
#17897=CARTESIAN_POINT ( 'NONE',  ( -57.36042740578360366, 3.725040285533370632, -1.239922660687675871 ) ) ;
#17900=CARTESIAN_POINT ( 'NONE',  ( -59.29999999999999716, -3.581647374645368309, -0.5069159045576940859 ) ) ;
#17905=DIRECTION ( 'NONE',  ( 1.000000000000000000, 3.054025858079668409E-16, -2.042474015755241579E-16 ) ) ;
#17914=CIRCLE ( 'NONE', #2749, 1.474417381223824153 ) ;
#17918=CARTESIAN_POINT ( 'NONE',  ( -54.49999999999998579, 3.724034196517557405, 0.2473046399340681489 ) ) ;
#17930=ORIENTED_EDGE ( 'NONE', *, *, #2864, .T. ) ;
#17945=CARTESIAN_POINT ( 'NONE',  ( -57.34599364905385954, 0.2309624077929011976, 3.875409454552789956 ) ) ;
#17946=CYLINDRICAL_SURFACE ( 'NONE', #89, 3.750000000000000444 ) ;
#17959=DIRECTION ( 'NONE',  ( -1.000000000000000000, -3.054025858079668409E-16, 2.042474015755241579E-16 ) ) ;
#17966=CARTESIAN_POINT ( 'NONE',  ( -58.42292740578360366, -3.330682475591783653, -0.6830477631804107164 ) ) ;
#17979=ADVANCED_FACE ( 'NONE', ( #23184, #5758 ), #13040, .T. ) ;
#17984=EDGE_CURVE ( 'NONE', #22862, #18443, #26177, .T. ) ;
#17986=CARTESIAN_POINT ( 'NONE',  ( -57.69184846062113081, 0.2309624077929080255, 3.875409454552792177 ) ) ;
#18003=ORIENTED_EDGE ( 'NONE', *, *, #26514, .T. ) ;
#18009=CARTESIAN_POINT ( 'NONE',  ( -54.47085481156724285, -3.673546848079175309, -0.7533615035078072841 ) ) ;
#18029=EDGE_CURVE ( 'NONE', #23231, #11632, #10808, .T. ) ;
#18033=AXIS2_PLACEMENT_3D ( 'NONE', #21209, #3757, #6465 ) ;
#18040=DIRECTION ( 'NONE',  ( 1.000000000000000000, 3.054025858079668409E-16, -2.042474015755241579E-16 ) ) ;
#18051=VERTEX_POINT ( 'NONE', #23330 ) ;
#18057=EDGE_LOOP ( 'NONE', ( #20171, #27717, #14029, #25045 ) ) ;
#18059=TOROIDAL_SURFACE ( 'NONE', #31200, 2.050000000000000266, 0.05000000000000000278 ) ;
#18066=CARTESIAN_POINT ( 'NONE',  ( -59.36042740578360366, -0.7887156198831606346, 3.845940847736174284 ) ) ;
#18072=( NAMED_UNIT ( * ) SI_UNIT ( $, .STERADIAN. ) SOLID_ANGLE_UNIT ( ) );
#18128=CARTESIAN_POINT ( 'NONE',  ( -57.72499999999998010, 4.751120590182407177, 0.9743475445367628662 ) ) ;
#18151=( BOUNDED_SURFACE ( )  B_SPLINE_SURFACE ( 1, 2, ( 
 ( #17591, #7463, #22490, #3167, #12809, #17134, #26779, #788, #29767, #5084, #19666, #14734, #22034, #330, #29303, #5228, #17275, #26917, #14877, #24539, #2858, #12508, #25175, #11075, #22960, #30065, #28170, #20604, #8541, #3494, #1415, #25473, #27863, #30528, #1250, #3782, #13131, #30233, #15971, #13421, #6177, #963, #18226, #12978, #1108, #10613, #20756, #25795, #15822, #17897, #23127, #27533, #10911, #6486, #30384, #10758, #8686, #28005, #8834, #1565, #16146, #18367, #6320, #13271, #25636, #22666, #22820, #3949, #13589, #8380, #23279, #8230, #20291, #18526, #29920, #11224, #20898, #15682, #5859, #15522, #20440, #18066, #27709, #6031, #25328, #3637, #31010, #16304, #23899, #16628, #19000, #21703, #23751, #26271, #4251, #21386, #7120, #4577, #28649, #23428, #11705, #4103, #23588, #1710, #11855, #16928, #6967, #9014, #14225 ),
 ( #26423, #4719, #12027, #28335, #16779, #14376, #11378, #21233, #21063, #2191, #24047, #28486, #21533, #30865, #13895, #1891, #31175, #30707, #9508, #9331, #13743, #2043, #2358, #6792, #14141, #19169, #9182, #28809, #18844, #9662, #19316, #28952, #18686, #6640, #25949, #7260, #11556, #16451, #26108, #4423, #14069, #14551, #27204, #29560, #7875, #24671, #5513, #15168, #3136, #9957, #2527, #24362, #12309, #597, #22458, #288, #7722, #17552, #7584, #2984, #2813, #19632, #24822, #29271, #17383, #753, #26572, #4885, #9796, #24502, #24215, #5338, #20098, #26883, #10414, #19464, #17244, #10259, #29732, #10111, #8046, #12777, #12176, #5193, #21857, #144, #29109, #29414, #2673, #27030, #15003, #12627, #7426, #12468, #22312, #19928, #14841, #22160, #17100, #26748, #5048, #448, #14701, #21996, #19778, #16225, #23353, #5824, #18447 ) ),
 .UNSPECIFIED., .F., .F., .F. ) 
 B_SPLINE_SURFACE_WITH_KNOTS ( ( 2, 2 ),
 ( 3, 2, 2, 2, 2, 2, 2, 2, 2, 2, 2, 2, 2, 2, 2, 2, 2, 2, 2, 2, 2, 2, 2, 2, 2, 2, 2, 2, 2, 2, 2, 2, 2, 2, 2, 2, 2, 2, 2, 2, 2, 2, 2, 2, 2, 2, 2, 2, 2, 2, 2, 2, 2, 2, 3 ),
 ( 0.000000000000000000, 1.000000000000000000 ),
 ( 0.000000000000000000, 0.01851851851851851749, 0.03703703703703703498, 0.05555555555555555247, 0.07407407407407406996, 0.09259259259259258745, 0.1111111111111111049, 0.1296296296296296224, 0.1481481481481481399, 0.1666666666666666574, 0.1851851851851851749, 0.2037037037037036924, 0.2222222222222222099, 0.2407407407407407274, 0.2592592592592592449, 0.2777777777777777901, 0.2962962962962962798, 0.3148148148148148251, 0.3333333333333333148, 0.3518518518518518601, 0.3703703703703703498, 0.3888888888888888951, 0.4074074074074073848, 0.4259259259259259300, 0.4444444444444444198, 0.4629629629629629650, 0.4814814814814814548, 0.5000000000000000000, 0.5185185185185184897, 0.5370370370370370905, 0.5555555555555555802, 0.5740740740740740700, 0.5925925925925925597, 0.6111111111111111605, 0.6296296296296296502, 0.6481481481481481399, 0.6666666666666666297, 0.6851851851851852304, 0.7037037037037037202, 0.7222222222222222099, 0.7407407407407406996, 0.7592592592592593004, 0.7777777777777777901, 0.7962962962962962798, 0.8148148148148147696, 0.8333333333333333703, 0.8518518518518518601, 0.8703703703703703498, 0.8888888888888888395, 0.9074074074074074403, 0.9259259259259259300, 0.9444444444444444198, 0.9629629629629629095, 0.9814814814814815103, 1.000000000000000000 ),
 .UNSPECIFIED. ) 
 GEOMETRIC_REPRESENTATION_ITEM ( )  RATIONAL_B_SPLINE_SURFACE ( (
 ( 1.000000000000000000, 0.8660254037844387076, 1.000000000000000000, 0.8660254037844387076, 1.000000000000000000, 0.8660254037844387076, 1.000000000000000000, 0.8660254037844387076, 1.000000000000000000, 0.8660254037844387076, 1.000000000000000000, 0.8660254037844387076, 1.000000000000000000, 0.8660254037844387076, 1.000000000000000000, 0.8660254037844387076, 1.000000000000000000, 0.8660254037844387076, 1.000000000000000000, 0.8660254037844387076, 1.000000000000000000, 0.8660254037844387076, 1.000000000000000000, 0.8660254037844387076, 1.000000000000000000, 0.8660254037844387076, 1.000000000000000000, 0.8660254037844387076, 1.000000000000000000, 0.8660254037844387076, 1.000000000000000000, 0.8660254037844387076, 1.000000000000000000, 0.8660254037844387076, 1.000000000000000000, 0.8660254037844387076, 1.000000000000000000, 0.8660254037844387076, 1.000000000000000000, 0.8660254037844387076, 1.000000000000000000, 0.8660254037844387076, 1.000000000000000000, 0.8660254037844387076, 1.000000000000000000, 0.8660254037844387076, 1.000000000000000000, 0.8660254037844387076, 1.000000000000000000, 0.8660254037844387076, 1.000000000000000000, 0.8660254037844387076, 1.000000000000000000, 0.8660254037844387076, 1.000000000000000000, 0.8660254037844387076, 1.000000000000000000, 0.8660254037844387076, 1.000000000000000000, 0.8660254037844387076, 1.000000000000000000, 0.8660254037844387076, 1.000000000000000000, 0.8660254037844387076, 1.000000000000000000, 0.8660254037844387076, 1.000000000000000000, 0.8660254037844387076, 1.000000000000000000, 0.8660254037844387076, 1.000000000000000000, 0.8660254037844387076, 1.000000000000000000, 0.8660254037844387076, 1.000000000000000000, 0.8660254037844387076, 1.000000000000000000, 0.8660254037844387076, 1.000000000000000000, 0.8660254037844387076, 1.000000000000000000, 0.8660254037844387076, 1.000000000000000000, 0.8660254037844387076, 1.000000000000000000, 0.8660254037844387076, 1.000000000000000000, 0.8660254037844387076, 1.000000000000000000, 0.8660254037844387076, 1.000000000000000000, 0.8660254037844387076, 1.000000000000000000, 0.8660254037844387076, 1.000000000000000000, 0.8660254037844387076, 1.000000000000000000, 0.8660254037844387076, 1.000000000000000000, 0.8660254037844387076, 1.000000000000000000, 0.8660254037844387076, 1.000000000000000000, 0.8660254037844387076, 1.000000000000000000, 0.8660254037844387076, 1.000000000000000000, 0.8660254037844387076, 1.000000000000000000),
 ( 1.000000000000000000, 0.8660254037844387076, 1.000000000000000000, 0.8660254037844387076, 1.000000000000000000, 0.8660254037844387076, 1.000000000000000000, 0.8660254037844387076, 1.000000000000000000, 0.8660254037844387076, 1.000000000000000000, 0.8660254037844387076, 1.000000000000000000, 0.8660254037844387076, 1.000000000000000000, 0.8660254037844387076, 1.000000000000000000, 0.8660254037844387076, 1.000000000000000000, 0.8660254037844387076, 1.000000000000000000, 0.8660254037844387076, 1.000000000000000000, 0.8660254037844387076, 1.000000000000000000, 0.8660254037844387076, 1.000000000000000000, 0.8660254037844387076, 1.000000000000000000, 0.8660254037844387076, 1.000000000000000000, 0.8660254037844387076, 1.000000000000000000, 0.8660254037844387076, 1.000000000000000000, 0.8660254037844387076, 1.000000000000000000, 0.8660254037844387076, 1.000000000000000000, 0.8660254037844387076, 1.000000000000000000, 0.8660254037844387076, 1.000000000000000000, 0.8660254037844387076, 1.000000000000000000, 0.8660254037844387076, 1.000000000000000000, 0.8660254037844387076, 1.000000000000000000, 0.8660254037844387076, 1.000000000000000000, 0.8660254037844387076, 1.000000000000000000, 0.8660254037844387076, 1.000000000000000000, 0.8660254037844387076, 1.000000000000000000, 0.8660254037844387076, 1.000000000000000000, 0.8660254037844387076, 1.000000000000000000, 0.8660254037844387076, 1.000000000000000000, 0.8660254037844387076, 1.000000000000000000, 0.8660254037844387076, 1.000000000000000000, 0.8660254037844387076, 1.000000000000000000, 0.8660254037844387076, 1.000000000000000000, 0.8660254037844387076, 1.000000000000000000, 0.8660254037844387076, 1.000000000000000000, 0.8660254037844387076, 1.000000000000000000, 0.8660254037844387076, 1.000000000000000000, 0.8660254037844387076, 1.000000000000000000, 0.8660254037844387076, 1.000000000000000000, 0.8660254037844387076, 1.000000000000000000, 0.8660254037844387076, 1.000000000000000000, 0.8660254037844387076, 1.000000000000000000, 0.8660254037844387076, 1.000000000000000000, 0.8660254037844387076, 1.000000000000000000, 0.8660254037844387076, 1.000000000000000000, 0.8660254037844387076, 1.000000000000000000, 0.8660254037844387076, 1.000000000000000000, 0.8660254037844387076, 1.000000000000000000, 0.8660254037844387076, 1.000000000000000000, 0.8660254037844387076, 1.000000000000000000, 0.8660254037844387076, 1.000000000000000000, 0.8660254037844387076, 1.000000000000000000) ) ) 
 REPRESENTATION_ITEM ( '' )  SURFACE ( )  );
#18158=CYLINDRICAL_SURFACE ( 'NONE', #30336, 3.750000000000000444 ) ;
#18170=CIRCLE ( 'NONE', #26753, 4.849999999999999645 ) ;
#18180=CARTESIAN_POINT ( 'NONE',  ( -58.22085481156723574, -3.673546848079176197, -0.7533615035078065070 ) ) ;
#18202=CARTESIAN_POINT ( 'NONE',  ( -54.73542740578361077, -3.725040285533364859, 1.239922660687674760 ) ) ;
#18219=ORIENTED_EDGE ( 'NONE', *, *, #5080, .T. ) ;
#18225=LINE ( 'NONE', #6484, #31219 ) ;
#18226=CARTESIAN_POINT ( 'NONE',  ( -56.92292740578359656, -3.330682475591783209, -0.6830477631804109384 ) ) ;
#18231=ORIENTED_EDGE ( 'NONE', *, *, #21785, .T. ) ;
#18253=ORIENTED_EDGE ( 'NONE', *, *, #10926, .T. ) ;
#18282=ORIENTED_EDGE ( 'NONE', *, *, #20261, .F. ) ;
#18283=DIRECTION ( 'NONE',  ( -2.581436205204234499E-16, 0.9796124928211140670, 0.2008964009354147762 ) ) ;
#18294=AXIS2_PLACEMENT_3D ( 'NONE', #15760, #28094, #16233 ) ;
#18300=CARTESIAN_POINT ( 'NONE',  ( -69.18535533905931345, -6.887031541980249260E-16, 2.444420817412074983E-15 ) ) ;
#18325=CARTESIAN_POINT ( 'NONE',  ( -59.15835481156722864, -0.8699069336946633202, 4.241846523238430144 ) ) ;
#18347=CARTESIAN_POINT ( 'NONE',  ( -58.61042740578360366, -0.7887156198831720699, 3.845940847736171619 ) ) ;
#18348=CARTESIAN_POINT ( 'NONE',  ( -56.59585481156723574, -1.184343223768586251, -3.558065644182725862 ) ) ;
#18351=FACE_OUTER_BOUND ( 'NONE', #23849, .T. ) ;
#18365=CARTESIAN_POINT ( 'NONE',  ( -55.47085481156723574, 1.184343223768591580, 3.558065644182726750 ) ) ;
#18367=CARTESIAN_POINT ( 'NONE',  ( -58.11042740578360366, 3.725040285533370632, -1.239922660687675871 ) ) ;
#18374=ORIENTED_EDGE ( 'NONE', *, *, #1113, .T. ) ;
#18382=CARTESIAN_POINT ( 'NONE',  ( -55.03335481156724995, 0.7533615035078067290, -3.673546848079180194 ) ) ;
#18388=CARTESIAN_POINT ( 'NONE',  ( -54.49999999999997868, 3.712072993515388664, 0.5023824248525554648 ) ) ;
#18412=EDGE_CURVE ( 'NONE', #6633, #9415, #16453, .T. ) ;
#18426=CARTESIAN_POINT ( 'NONE',  ( -55.74999999999997158, -2.489203624310587948, 2.804704140674914026 ) ) ;
#18431=CARTESIAN_POINT ( 'NONE',  ( -59.29999999999996163, 1.763130761670032021, 3.204107478254790919 ) ) ;
#18443=VERTEX_POINT ( 'NONE', #11237 ) ;
#18447=CARTESIAN_POINT ( 'NONE',  ( -61.24999999999996447, 3.673546848079179750, 0.7533615035078069511 ) ) ;
#18448=ORIENTED_EDGE ( 'NONE', *, *, #15191, .T. ) ;
#18451=VECTOR ( 'NONE', #8462, 1000.000000000000000 ) ;
#18462=DIRECTION ( 'NONE',  ( 0.000000000000000000, -0.2008964009354147484, 0.9796124928211139560 ) ) ;
#18463=PLANE ( 'NONE',  #4514 ) ;
#18480=CARTESIAN_POINT ( 'NONE',  ( -59.28335481156722864, 3.238593381231847257, 2.874284765127022911 ) ) ;
#18495=FILL_AREA_STYLE_COLOUR ( '', #29601 ) ;
#18499=AXIS2_PLACEMENT_3D ( 'NONE', #692, #24912, #10527 ) ;
#18502=CIRCLE ( 'NONE', #25558, 0.5000000000000013323 ) ;
#18503=CARTESIAN_POINT ( 'NONE',  ( -56.86042740578360366, -2.936324665650192234, -2.606018187048508850 ) ) ;
#18505=( BOUNDED_CURVE ( )  B_SPLINE_CURVE ( 2, ( #8176, #10850, #12907, #15453, #3107, #20233, #27647, #13074, #17843 ),
 .UNSPECIFIED., .F., .T. ) 
 B_SPLINE_CURVE_WITH_KNOTS ( ( 3, 2, 2, 2, 3 ),
 ( 0.6388888888888889506, 0.6481481481481481399, 0.6666666666666666297, 0.6851851851851852304, 0.6944444444444445308 ),
 .UNSPECIFIED. ) 
 CURVE ( )  GEOMETRIC_REPRESENTATION_ITEM ( )  RATIONAL_B_SPLINE_CURVE ( ( 0.9330127018922194093, 0.9330127018922197424, 1.000000000000000000, 0.8660254037844387076, 1.000000000000000000, 0.8660254037844387076, 1.000000000000000000, 0.9330127018922189652, 0.9330127018922194093 ) ) 
 REPRESENTATION_ITEM ( '' )  );
#18521=AXIS2_PLACEMENT_3D ( 'NONE', #14598, #24552, #2576 ) ;
#18524=CARTESIAN_POINT ( 'NONE',  ( -55.59585481156724285, 3.673546848079182414, 0.7533615035078059519 ) ) ;
#18526=CARTESIAN_POINT ( 'NONE',  ( -58.86042740578360366, 3.725040285533370632, -1.239922660687675648 ) ) ;
#18529=CARTESIAN_POINT ( 'NONE',  ( -60.49999999999996447, 3.526604974156013039, 0.7232270433674945487 ) ) ;
#18549=AXIS2_PLACEMENT_3D ( 'NONE', #8664, #18819, #23727 ) ;
#18558=EDGE_CURVE ( 'NONE', #29802, #21265, #14398, .T. ) ;
#18588=DIRECTION ( 'NONE',  ( 1.000000000000000000, 3.054027077731387480E-16, -2.042479963029832083E-16 ) ) ;
#18592=CARTESIAN_POINT ( 'NONE',  ( -56.72499999999997300, 3.116721586436802063E-15, -1.005743832985040150E-16 ) ) ;
#18601=CIRCLE ( 'NONE', #4938, 0.04999999999999989175 ) ;
#18610=ORIENTED_EDGE ( 'NONE', *, *, #15291, .T. ) ;
#18619=CONICAL_SURFACE ( 'NONE', #7002, 2.765000000000001013, 0.03997868712329009228 ) ;
#18625=CARTESIAN_POINT ( 'NONE',  ( -57.97085481156723574, 2.489203624310592389, -2.804704140674918911 ) ) ;
#18627=FACE_BOUND ( 'NONE', #5322, .T. ) ;
#18637=ORIENTED_EDGE ( 'NONE', *, *, #20143, .F. ) ;
#18641=CARTESIAN_POINT ( 'NONE',  ( -58.65835481156723574, 4.108500314926515351, -1.367561758111407899 ) ) ;
#18661=( BOUNDED_CURVE ( )  B_SPLINE_CURVE ( 2, ( #19467, #9183, #23753, #24049, #6969 ),
 .UNSPECIFIED., .F., .T. ) 
 B_SPLINE_CURVE_WITH_KNOTS ( ( 3, 2, 3 ),
 ( 0.06011924821131572894, 0.07407407407407406996, 0.08333333333333332871 ),
 .UNSPECIFIED. ) 
 CURVE ( )  GEOMETRIC_REPRESENTATION_ITEM ( )  RATIONAL_B_SPLINE_CURVE ( ( 0.9502399529286075230, 0.8990420233480378442, 1.000000000000000000, 0.9330127018922194093, 0.9330127018922194093 ) ) 
 REPRESENTATION_ITEM ( '' )  );
#18663=CARTESIAN_POINT ( 'NONE',  ( -56.29792740578360366, -2.256877952708266299, 2.542931754211921191 ) ) ;
#18671=EDGE_CURVE ( 'NONE', #4537, #15739, #6007, .T. ) ;
#18672=DIRECTION ( 'NONE',  ( 0.9990482215818580203, -0.008762977932701932968, 0.04273009679227924434 ) ) ;
#18686=CARTESIAN_POINT ( 'NONE',  ( -56.49999999999997158, -2.489203624310585283, 2.804704140674916690 ) ) ;
#18701=ADVANCED_FACE ( 'NONE', ( #1228 ), #10890, .T. ) ;
#18719=EDGE_LOOP ( 'NONE', ( #15724, #24806, #29995, #2427 ) ) ;
#18723=EDGE_LOOP ( 'NONE', ( #143, #27750, #8186, #785 ) ) ;
#18741=DIRECTION ( 'NONE',  ( -1.000000000000000000, -3.054025858079668409E-16, 2.042474015755241579E-16 ) ) ;
#18756=DIRECTION ( 'NONE',  ( -2.614375865348240525E-16, 0.2008964009354147762, -0.9796124928211140670 ) ) ;
#18760=CARTESIAN_POINT ( 'NONE',  ( -60.92292740578359656, 1.073804522883521351, 3.225979517392337570 ) ) ;
#18782=FACE_OUTER_BOUND ( 'NONE', #9061, .T. ) ;
#18788=CARTESIAN_POINT ( 'NONE',  ( -56.06249999999997868, 4.108500314926513575, -1.367561758111403680 ) ) ;
#18798=CARTESIAN_POINT ( 'NONE',  ( -56.03335481156723574, -4.108500314926510022, 1.367561758111407455 ) ) ;
#18799=CARTESIAN_POINT ( 'NONE',  ( -56.67499999999996874, 3.131991715727200307E-15, -1.107867533772800737E-16 ) ) ;
#18805=CARTESIAN_POINT ( 'NONE',  ( -67.99999999999995737, -3.266925685480207642E-16, 2.202315069465528948E-15 ) ) ;
#18808=DIRECTION ( 'NONE',  ( 2.581436205204234006E-16, -0.9796124928211140670, -0.2008964009354148872 ) ) ;
#18810=DIRECTION ( 'NONE',  ( 1.000000000000000000, 3.054025858079668409E-16, -2.042474015755241579E-16 ) ) ;
#18819=DIRECTION ( 'NONE',  ( 1.000000000000000000, 3.054025858079668409E-16, -2.042474015755241579E-16 ) ) ;
#18821=CARTESIAN_POINT ( 'NONE',  ( -56.42292740578360366, 1.073804522883514689, 3.225979517392338902 ) ) ;
#18844=CARTESIAN_POINT ( 'NONE',  ( -56.24999999999997158, -1.184343223768585363, -3.558065644182724085 ) ) ;
#18872=VERTEX_POINT ( 'NONE', #26087 ) ;
#18873=ORIENTED_EDGE ( 'NONE', *, *, #3255, .T. ) ;
#18879=DIRECTION ( 'NONE',  ( -1.000000000000000000, -3.054025858079668409E-16, 2.042474015755241579E-16 ) ) ;
#18883=EDGE_LOOP ( 'NONE', ( #12211, #27316, #23930, #2536 ) ) ;
#18915=EDGE_CURVE ( 'NONE', #14055, #17250, #14421, .T. ) ;
#18917=AXIS2_PLACEMENT_3D ( 'NONE', #25679, #28040, #15562 ) ;
#18931=EDGE_CURVE ( 'NONE', #4965, #6063, #29112, .T. ) ;
#18951=CARTESIAN_POINT ( 'NONE',  ( -54.61042740578360366, -2.936324665650200672, -2.606018187048499080 ) ) ;
#18958=ORIENTED_EDGE ( 'NONE', *, *, #23780, .T. ) ;
#18974=CARTESIAN_POINT ( 'NONE',  ( -56.15835481156722153, -0.7533615035077977362, 3.673546848079179750 ) ) ;
#18976=CARTESIAN_POINT ( 'NONE',  ( -58.36042740578360366, -2.936324665650199783, -2.606018187048499524 ) ) ;
#18995=CARTESIAN_POINT ( 'NONE',  ( -60.54800159808252147, -0.7228413094357338808, 3.524724055549729229 ) ) ;
#19000=CARTESIAN_POINT ( 'NONE',  ( -59.92292740578359656, -3.330682475591783653, -0.6830477631804103833 ) ) ;
#19016=CARTESIAN_POINT ( 'NONE',  ( -55.22085481156723574, -3.673546848079175753, -0.7533615035078071731 ) ) ;
#19017=CARTESIAN_POINT ( 'NONE',  ( -68.01382336603234080, -3.309142602788800391E-16, 2.205138456058669928E-15 ) ) ;
#19023=FACE_OUTER_BOUND ( 'NONE', #26493, .T. ) ;
#19026=CARTESIAN_POINT ( 'NONE',  ( -59.29999999999997584, -0.7533615035078030653, 3.673546848079178417 ) ) ;
#19033=( GEOMETRIC_REPRESENTATION_CONTEXT ( 3 ) GLOBAL_UNCERTAINTY_ASSIGNED_CONTEXT ( ( #619 ) ) GLOBAL_UNIT_ASSIGNED_CONTEXT ( ( #17870, #20872, #15486 ) ) REPRESENTATION_CONTEXT ( 'NONE', 'WORKASPACE' ) );
#19050=CARTESIAN_POINT ( 'NONE',  ( -57.62499999999997158, 2.489203624310596830, -2.804704140674912249 ) ) ;
#19055=VECTOR ( 'NONE', #11238, 1000.000000000000000 ) ;
#19067=CARTESIAN_POINT ( 'NONE',  ( -58.84599364905385954, 0.2309624077928955632, 3.875409454552791289 ) ) ;
#19080=ORIENTED_EDGE ( 'NONE', *, *, #10614, .F. ) ;
#19095=ORIENTED_EDGE ( 'NONE', *, *, #28459, .T. ) ;
#19096=CIRCLE ( 'NONE', #5925, 0.04999999999999989175 ) ;
#19098=CARTESIAN_POINT ( 'NONE',  ( -59.30000000000042348, -2.541725022351402963, -2.757196748647571027 ) ) ;
#19110=AXIS2_PLACEMENT_3D ( 'NONE', #14891, #24553, #5097 ) ;
#19118=CARTESIAN_POINT ( 'NONE',  ( -56.61042740578360366, 3.725040285533371076, -1.239922660687675871 ) ) ;
#19134=DIRECTION ( 'NONE',  ( 0.000000000000000000, -0.2008964009354147484, 0.9796124928211139560 ) ) ;
#19169=CARTESIAN_POINT ( 'NONE',  ( -56.06249999999997868, 4.108500314926511798, -1.367561758111407677 ) ) ;
#19172=CIRCLE ( 'NONE', #31280, 4.849999999999999645 ) ;
#19200=ORIENTED_EDGE ( 'NONE', *, *, #25069, .T. ) ;
#19204=CARTESIAN_POINT ( 'NONE',  ( -71.49999999999998579, -0.3062499654112579295, 1.493338310920507839 ) ) ;
#19220=ADVANCED_FACE ( 'NONE', ( #27952 ), #13439, .T. ) ;
#19236=ADVANCED_FACE ( 'NONE', ( #6434 ), #25598, .F. ) ;
#19252=ORIENTED_EDGE ( 'NONE', *, *, #26030, .T. ) ;
#19253=CIRCLE ( 'NONE', #26305, 0.05000000000000009298 ) ;
#19274=CARTESIAN_POINT ( 'NONE',  ( -59.72085481156722864, -3.673546848079176197, -0.7533615035078060629 ) ) ;
#19285=DIRECTION ( 'NONE',  ( 0.000000000000000000, 0.2008964009354147484, -0.9796124928211140670 ) ) ;
#19296=EDGE_CURVE ( 'NONE', #76, #9362, #4352, .T. ) ;
#19314=CARTESIAN_POINT ( 'NONE',  ( -60.48535533905928219, -0.8667965836981817995, 4.226679811941401965 ) ) ;
#19316=CARTESIAN_POINT ( 'NONE',  ( -56.37499999999997158, -3.673546848079173532, -0.7533615035078063960 ) ) ;
#19317=DIRECTION ( 'NONE',  ( 1.000000000000000000, 3.054025858079668409E-16, -2.042474015755241579E-16 ) ) ;
#19327=CARTESIAN_POINT ( 'NONE',  ( -58.81249999999996447, -0.7533615035078081723, 3.673546848079176197 ) ) ;
#19343=UNCERTAINTY_MEASURE_WITH_UNIT (LENGTH_MEASURE( 1.000000000000000082E-05 ), #24746, 'distance_accuracy_value', 'NONE');
#19350=( BOUNDED_CURVE ( )  B_SPLINE_CURVE ( 2, ( #23065, #19067, #12093, #6861, #21771, #1363, #11176, #31251, #11030 ),
 .UNSPECIFIED., .F., .T. ) 
 B_SPLINE_CURVE_WITH_KNOTS ( ( 3, 2, 2, 2, 3 ),
 ( 0.6388888888888889506, 0.6481481481481481399, 0.6666666666666666297, 0.6851851851851852304, 0.6944444444444445308 ),
 .UNSPECIFIED. ) 
 CURVE ( )  GEOMETRIC_REPRESENTATION_ITEM ( )  RATIONAL_B_SPLINE_CURVE ( ( 0.9330127018922194093, 0.9330127018922197424, 1.000000000000000000, 0.8660254037844387076, 1.000000000000000000, 0.8660254037844387076, 1.000000000000000000, 0.9330127018922189652, 0.9330127018922194093 ) ) 
 REPRESENTATION_ITEM ( '' )  );
#19359=ADVANCED_FACE ( 'NONE', ( #653 ), #21056, .T. ) ;
#19379=CARTESIAN_POINT ( 'NONE',  ( -71.44999999999998863, -1.380331489585512972E-15, 2.906968604901091669E-15 ) ) ;
#19418=CARTESIAN_POINT ( 'NONE',  ( -60.22085481156723574, 2.489203624310591945, -2.804704140674918467 ) ) ;
#19464=CARTESIAN_POINT ( 'NONE',  ( -59.18749999999996447, 0.8699069336946683162, -4.241846523238426592 ) ) ;
#19466=CARTESIAN_POINT ( 'NONE',  ( -57.22499999999997300, -0.9241234443029057166, 4.506217466977124886 ) ) ;
#19467=CARTESIAN_POINT ( 'NONE',  ( -54.49999999999997158, -3.745083032500879039, 0.1919715595446555012 ) ) ;
#19471=FACE_OUTER_BOUND ( 'NONE', #5537, .T. ) ;
#19474=EDGE_CURVE ( 'NONE', #5081, #22862, #29829, .T. ) ;
#19482=CARTESIAN_POINT ( 'NONE',  ( -56.74999999999997158, 3.673546848079180638, 0.7533615035078086164 ) ) ;
#19493=ORIENTED_EDGE ( 'NONE', *, *, #30930, .T. ) ;
#19517=AXIS2_PLACEMENT_3D ( 'NONE', #12155, #7403, #19760 ) ;
#19522=CIRCLE ( 'NONE', #23561, 4.800000000000000711 ) ;
#19534=DIRECTION ( 'NONE',  ( 0.000000000000000000, -0.2008964009354147484, 0.9796124928211139560 ) ) ;
#19543=ORIENTED_EDGE ( 'NONE', *, *, #22679, .T. ) ;
#19557=EDGE_LOOP ( 'NONE', ( #29799, #29218, #28159, #15345 ) ) ;
#19585=CARTESIAN_POINT ( 'NONE',  ( -55.61042740578361077, -0.7887156198831598575, 3.845940847736173840 ) ) ;
#19589=VERTEX_POINT ( 'NONE', #28508 ) ;
#19610=DIRECTION ( 'NONE',  ( -1.000000000000000000, -3.054025858079668409E-16, 2.042474015755241579E-16 ) ) ;
#19632=CARTESIAN_POINT ( 'NONE',  ( -58.31249999999997158, 4.108500314926511798, -1.367561758111407011 ) ) ;
#19654=CARTESIAN_POINT ( 'NONE',  ( -54.54999999999998295, 3.780972210569126836E-15, -5.448124817252668230E-16 ) ) ;
#19666=CARTESIAN_POINT ( 'NONE',  ( -54.92292740578361077, 1.073804522883522239, 3.225979517392335794 ) ) ;
#19679=AXIS2_PLACEMENT_3D ( 'NONE', #6089, #18283, #30598 ) ;
#19704=DIRECTION ( 'NONE',  ( 2.581436205204234006E-16, -0.9796124928211140670, -0.2008964009354148872 ) ) ;
#19706=EDGE_LOOP ( 'NONE', ( #18282, #2303, #20239, #27558 ) ) ;
#19738=CARTESIAN_POINT ( 'NONE',  ( -60.17292740578359656, 1.073804522883521351, 3.225979517392337126 ) ) ;
#19751=DIRECTION ( 'NONE',  ( -2.614375865348240525E-16, 0.2008964009354147762, -0.9796124928211140670 ) ) ;
#19760=DIRECTION ( 'NONE',  ( 0.000000000000000000, 0.2008964009354147762, -0.9796124928211139560 ) ) ;
#19767=EDGE_LOOP ( 'NONE', ( #6858, #11879, #26663, #547 ) ) ;
#19770=CARTESIAN_POINT ( 'NONE',  ( -58.78335481156722864, 0.7533615035077975142, -3.673546848079180638 ) ) ;
#19778=CARTESIAN_POINT ( 'NONE',  ( -60.99999999999996447, -2.489203624310586171, 2.804704140674918023 ) ) ;
#19780=CARTESIAN_POINT ( 'NONE',  ( -55.31249999999997868, 4.108500314926513575, -1.367561758111404790 ) ) ;
#19785=DIRECTION ( 'NONE',  ( 0.000000000000000000, 0.2008964009354147762, -0.9796124928211140670 ) ) ;
#19792=CARTESIAN_POINT ( 'NONE',  ( -56.68749999999997158, 3.238593381231837487, 2.874284765127031349 ) ) ;
#19802=VERTEX_POINT ( 'NONE', #16902 ) ;
#19815=CARTESIAN_POINT ( 'NONE',  ( -59.29999999999996163, -3.390200327460917595, 0.9814680162012726639 ) ) ;
#19817=ORIENTED_EDGE ( 'NONE', *, *, #3255, .F. ) ;
#19874=ORIENTED_EDGE ( 'NONE', *, *, #23282, .T. ) ;
#19878=CARTESIAN_POINT ( 'NONE',  ( -59.79792740578359656, -1.073804522883517576, -3.225979517392334905 ) ) ;
#19889=EDGE_CURVE ( 'NONE', #11624, #13819, #13967, .T. ) ;
#19928=CARTESIAN_POINT ( 'NONE',  ( -60.43749999999996447, 3.238593381231845481, 2.874284765127022023 ) ) ;
#19933=CARTESIAN_POINT ( 'NONE',  ( -54.72099364905386665, -0.2309624077929028074, -3.875409454552789956 ) ) ;
#19949=ADVANCED_FACE ( 'NONE', ( #20503 ), #30663, .F. ) ;
#19958=ORIENTED_EDGE ( 'NONE', *, *, #17370, .F. ) ;
#19964=EDGE_CURVE ( 'NONE', #3318, #31001, #28083, .T. ) ;
#19992=ORIENTED_EDGE ( 'NONE', *, *, #13652, .T. ) ;
#19999=ORIENTED_EDGE ( 'NONE', *, *, #18931, .F. ) ;
#20004=ORIENTED_EDGE ( 'NONE', *, *, #29405, .T. ) ;
#20021=CARTESIAN_POINT ( 'NONE',  ( -57.22085481156723574, 2.489203624310592389, -2.804704140674919355 ) ) ;
#20027=DIRECTION ( 'NONE',  ( -1.000000000000000000, -3.054025858079668409E-16, 2.042474015755241579E-16 ) ) ;
#20037=CARTESIAN_POINT ( 'NONE',  ( -57.17292740578359656, 1.073804522883521795, 3.225979517392336682 ) ) ;
#20047=VECTOR ( 'NONE', #29286, 1000.000000000000000 ) ;
#20052=AXIS2_PLACEMENT_3D ( 'NONE', #12260, #4822, #26688 ) ;
#20075=ORIENTED_EDGE ( 'NONE', *, *, #5613, .F. ) ;
#20083=CARTESIAN_POINT ( 'NONE',  ( -55.22085481156723574, -3.673546848079175753, -0.7533615035078071731 ) ) ;
#20098=CARTESIAN_POINT ( 'NONE',  ( -58.99999999999997158, 3.673546848079180638, 0.7533615035078062849 ) ) ;
#20099=CYLINDRICAL_SURFACE ( 'NONE', #21124, 3.750000000000000444 ) ;
#20101=CARTESIAN_POINT ( 'NONE',  ( -54.49999999999997158, -2.730644924724235700, -2.351390379901977745 ) ) ;
#20112=CARTESIAN_POINT ( 'NONE',  ( -55.17292740578361077, 2.256877952708270296, -2.542931754211924744 ) ) ;
#20122=DIRECTION ( 'NONE',  ( 0.000000000000000000, 0.2008964009354152203, -0.9796124928211138450 ) ) ;
#20143=EDGE_CURVE ( 'NONE', #9362, #76, #5315, .T. ) ;
#20147=ADVANCED_FACE ( 'NONE', ( #23481 ), #7846, .F. ) ;
#20171=ORIENTED_EDGE ( 'NONE', *, *, #13640, .F. ) ;
#20194=CARTESIAN_POINT ( 'NONE',  ( -56.94184846062112371, 0.2309624077929111619, 3.875409454552790844 ) ) ;
#20195=CARTESIAN_POINT ( 'NONE',  ( -54.65400635094609072, 1.737685414808520568, -3.471684241605565102 ) ) ;
#20207=PRODUCT ( 'Cap', 'Cap', '', ( #13591 ) ) ;
#20208=CARTESIAN_POINT ( 'NONE',  ( -59.11042740578359656, -2.936324665650201560, -2.606018187048497747 ) ) ;
#20211=EDGE_LOOP ( 'NONE', ( #4655, #9909, #5666, #23528 ) ) ;
#20212=ORIENTED_EDGE ( 'NONE', *, *, #2752, .T. ) ;
#20219=LINE ( 'NONE', #10545, #7600 ) ;
#20220=CIRCLE ( 'NONE', #28286, 2.050000000000000266 ) ;
#20233=CARTESIAN_POINT ( 'NONE',  ( -58.65835481156723574, 4.108500314926515351, -1.367561758111408121 ) ) ;
#20239=ORIENTED_EDGE ( 'NONE', *, *, #22754, .T. ) ;
#20256=ORIENTED_EDGE ( 'NONE', *, *, #23186, .T. ) ;
#20261=EDGE_CURVE ( 'NONE', #29380, #20706, #12908, .T. ) ;
#20291=CARTESIAN_POINT ( 'NONE',  ( -58.79792740578360366, 3.330682475591789427, 0.6830477631804110494 ) ) ;
#20296=FILL_AREA_STYLE ('',( #12664 ) ) ;
#20298=CIRCLE ( 'NONE', #22826, 0.05000000000000009298 ) ;
#20303=CARTESIAN_POINT ( 'NONE',  ( -57.77499999999997016, 2.796048871338436190E-15, 1.138853883557972617E-16 ) ) ;
#20309=CARTESIAN_POINT ( 'NONE',  ( -59.29999999999997584, -0.7533615035078030653, 3.673546848079178417 ) ) ;
#20310=CARTESIAN_POINT ( 'NONE',  ( -59.96464466094062828, 0.9714054848608624226, -4.736774497371789572 ) ) ;
#20313=VERTEX_POINT ( 'NONE', #23960 ) ;
#20320=ORIENTED_EDGE ( 'NONE', *, *, #21625, .T. ) ;
#20323=EDGE_LOOP ( 'NONE', ( #8333, #30810 ) ) ;
#20346=CARTESIAN_POINT ( 'NONE',  ( -54.49999999999997868, 3.796242339859525868E-15, -5.550248518040434488E-16 ) ) ;
#20353=TOROIDAL_SURFACE ( 'NONE', #8200, 4.600000000000000533, 0.5000000000000013323 ) ;
#20364=CARTESIAN_POINT ( 'NONE',  ( -59.54792740578360366, 3.330682475591789427, 0.6830477631804111605 ) ) ;
#20386=CARTESIAN_POINT ( 'NONE',  ( -58.81684846062111660, -0.2309624077929090247, -3.875409454552789512 ) ) ;
#20400=ORIENTED_EDGE ( 'NONE', *, *, #2460, .T. ) ;
#20440=CARTESIAN_POINT ( 'NONE',  ( -59.29792740578359656, -2.256877952708263635, 2.542931754211925188 ) ) ;
#20453=DIRECTION ( 'NONE',  ( -1.000000000000000000, -3.054025858079668409E-16, 2.042474015755241579E-16 ) ) ;
#20460=CARTESIAN_POINT ( 'NONE',  ( -54.50000000000000000, 2.751381343271932067, -2.278180102673284413 ) ) ;
#20496=CARTESIAN_POINT ( 'NONE',  ( -56.97085481156723574, 1.184343223768591136, 3.558065644182727194 ) ) ;
#20497=AXIS2_PLACEMENT_3D ( 'NONE', #27931, #25717, #23037 ) ;
#20503=FACE_OUTER_BOUND ( 'NONE', #29836, .T. ) ;
#20520=AXIS2_PLACEMENT_3D ( 'NONE', #18592, #14133, #28239 ) ;
#20527=CIRCLE ( 'NONE', #1774, 2.100000000000000089 ) ;
#20531=CARTESIAN_POINT ( 'NONE',  ( -59.29999999999997584, 2.330309927981285032E-15, 4.253626757584724400E-16 ) ) ;
#20533=DIRECTION ( 'NONE',  ( -1.000000000000000000, -3.054025858079668409E-16, 2.042474015755241579E-16 ) ) ;
#20604=CARTESIAN_POINT ( 'NONE',  ( -55.98542740578361077, 0.7887156198831667409, -3.845940847736174728 ) ) ;
#20605=CARTESIAN_POINT ( 'NONE',  ( -60.24999999999997868, 2.040177471463716435E-15, 6.193977072552205884E-16 ) ) ;
#20618=AXIS2_PLACEMENT_3D ( 'NONE', #16835, #2720, #10157 ) ;
#20622=DIRECTION ( 'NONE',  ( -1.000000000000000000, -3.054025858079668409E-16, 2.042474015755241579E-16 ) ) ;
#20635=CIRCLE ( 'NONE', #29210, 0.04999999999999989175 ) ;
#20659=DIRECTION ( 'NONE',  ( 1.000000000000000000, 3.054025858079668409E-16, -2.042474015755241579E-16 ) ) ;
#20667=CARTESIAN_POINT ( 'NONE',  ( -59.29999999999998295, 2.783937418660473728, 2.481186825065970769 ) ) ;
#20668=ORIENTED_EDGE ( 'NONE', *, *, #26816, .T. ) ;
#20706=VERTEX_POINT ( 'NONE', #13120 ) ;
#20710=CARTESIAN_POINT ( 'NONE',  ( -59.03335481156722864, -4.108500314926510022, 1.367561758111407899 ) ) ;
#20722=EDGE_CURVE ( 'NONE', #7502, #16804, #13286, .T. ) ;
#20729=SURFACE_STYLE_USAGE ( .BOTH. , #11199 ) ;
#20733=CARTESIAN_POINT ( 'NONE',  ( -57.79792740578359656, -2.256877952708268076, 2.542931754211920303 ) ) ;
#20735=CARTESIAN_POINT ( 'NONE',  ( -56.56684846062113081, -0.2309624077929025854, -3.875409454552791733 ) ) ;
#20756=CARTESIAN_POINT ( 'NONE',  ( -57.17292740578359656, 1.073804522883521795, 3.225979517392336682 ) ) ;
#20761=ORIENTED_EDGE ( 'NONE', *, *, #22642, .T. ) ;
#20778=CARTESIAN_POINT ( 'NONE',  ( -59.96464466094062828, 2.127325729886550933E-15, 5.611146207266455330E-16 ) ) ;
#20803=DIRECTION ( 'NONE',  ( 1.000000000000000000, 3.054027077731387480E-16, -2.042479963029832083E-16 ) ) ;
#20809=CARTESIAN_POINT ( 'NONE',  ( -59.29999999999999005, -1.394046907339186792, 3.175855595397861553 ) ) ;
#20830=DIRECTION ( 'NONE',  ( 1.000000000000000000, 3.054025858079668409E-16, -2.042474015755241579E-16 ) ) ;
#20844=AXIS2_PLACEMENT_3D ( 'NONE', #18529, #16632, #15974 ) ;
#20848=ORIENTED_EDGE ( 'NONE', *, *, #16340, .F. ) ;
#20852=EDGE_CURVE ( 'NONE', #27277, #9570, #30690, .T. ) ;
#20854=EDGE_LOOP ( 'NONE', ( #27357, #24256, #1068, #960 ) ) ;
#20857=CARTESIAN_POINT ( 'NONE',  ( -57.65835481156723574, -0.8699069336946629871, 4.241846523238430144 ) ) ;
#20862=ORIENTED_EDGE ( 'NONE', *, *, #23526, .F. ) ;
#20863=DIRECTION ( 'NONE',  ( 1.000000000000000000, 3.054025858079668409E-16, -2.042474015755241579E-16 ) ) ;
#20872=( NAMED_UNIT ( * ) PLANE_ANGLE_UNIT ( ) SI_UNIT ( $, .RADIAN. ) );
#20876=( BOUNDED_CURVE ( )  B_SPLINE_CURVE ( 2, ( #8277, #17945, #28379, #9380, #14280, #20947, #19050, #23945, #21284 ),
 .UNSPECIFIED., .F., .T. ) 
 B_SPLINE_CURVE_WITH_KNOTS ( ( 3, 2, 2, 2, 3 ),
 ( 0.4166666666666666852, 0.4259259259259259300, 0.4444444444444444198, 0.4629629629629629650, 0.4722222222222222654 ),
 .UNSPECIFIED. ) 
 CURVE ( )  GEOMETRIC_REPRESENTATION_ITEM ( )  RATIONAL_B_SPLINE_CURVE ( ( 0.9330127018922194093, 0.9330127018922195203, 1.000000000000000000, 0.8660254037844387076, 1.000000000000000000, 0.8660254037844387076, 1.000000000000000000, 0.9330127018922189652, 0.9330127018922194093 ) ) 
 REPRESENTATION_ITEM ( '' )  );
#20879=CARTESIAN_POINT ( 'NONE',  ( -58.42292740578360366, -3.330682475591780101, -0.6830477631804265926 ) ) ;
#20888=DIRECTION ( 'NONE',  ( 1.000000000000000000, 3.054025858079668409E-16, -2.042474015755241579E-16 ) ) ;
#20898=CARTESIAN_POINT ( 'NONE',  ( -59.04792740578360366, -1.073804522883517132, -3.225979517392335350 ) ) ;
#20906=DIRECTION ( 'NONE',  ( -1.000000000000000000, -3.054025858079668409E-16, 2.042474015755241579E-16 ) ) ;
#20930=DIRECTION ( 'NONE',  ( 0.000000000000000000, -0.2008964009354147484, 0.9796124928211139560 ) ) ;
#20947=CARTESIAN_POINT ( 'NONE',  ( -57.56249999999997158, 4.108500314926514463, -1.367561758111401238 ) ) ;
#20973=DIRECTION ( 'NONE',  ( 1.000000000000000000, 3.054025858079668409E-16, -2.042474015755241579E-16 ) ) ;
#20976=DIRECTION ( 'NONE',  ( -1.000000000000000000, -3.054025858079668409E-16, 2.042474015755241579E-16 ) ) ;
#21010=AXIS2_PLACEMENT_3D ( 'NONE', #10178, #5593, #12547 ) ;
#21011=CARTESIAN_POINT ( 'NONE',  ( -57.09585481156723574, 3.673546848079182414, 0.7533615035078063960 ) ) ;
#21042=CARTESIAN_POINT ( 'NONE',  ( -56.73542740578360366, 0.7887156198831762888, -3.845940847736172064 ) ) ;
#21056=TOROIDAL_SURFACE ( 'NONE', #11428, 1.524417381223824197, 0.05000000000000000278 ) ;
#21058=DIRECTION ( 'NONE',  ( 0.000000000000000000, -0.2008964009354147484, 0.9796124928211139560 ) ) ;
#21063=CARTESIAN_POINT ( 'NONE',  ( -54.99999999999997868, -2.489203624310585283, 2.804704140674916690 ) ) ;
#21072=ADVANCED_FACE ( 'NONE', ( #24489 ), #17228, .F. ) ;
#21076=CIRCLE ( 'NONE', #14043, 0.5000000000000013323 ) ;
#21124=AXIS2_PLACEMENT_3D ( 'NONE', #22630, #21998, #930 ) ;
#21128=DIRECTION ( 'NONE',  ( -1.000000000000000000, -3.054025858079668409E-16, 2.042474015755241579E-16 ) ) ;
#21140=CARTESIAN_POINT ( 'NONE',  ( -54.49999999999997868, 0.9643027244899942119, -4.702139965541348055 ) ) ;
#21158=DIRECTION ( 'NONE',  ( 0.000000000000000000, -0.2008964009354147762, 0.9796124928211140670 ) ) ;
#21168=DIRECTION ( 'NONE',  ( -1.000000000000000000, -3.054025858079668409E-16, 2.042474015755241579E-16 ) ) ;
#21187=CARTESIAN_POINT ( 'NONE',  ( -56.65835481156724285, -3.238593381231841928, -2.874284765127022467 ) ) ;
#21209=CARTESIAN_POINT ( 'NONE',  ( -60.48535533905928219, 1.968299342331293196E-15, 6.674684237050104391E-16 ) ) ;
#21211=CARTESIAN_POINT ( 'NONE',  ( -56.98542740578360366, -3.725040285533366191, 1.239922660687670986 ) ) ;
#21220=ORIENTED_EDGE ( 'NONE', *, *, #24488, .T. ) ;
#21233=CARTESIAN_POINT ( 'NONE',  ( -54.93749999999997158, -4.108500314926507357, 1.367561758111405901 ) ) ;
#21259=CARTESIAN_POINT ( 'NONE',  ( -67.99999999999997158, -3.266925685480267300E-16, 2.202315069465532498E-15 ) ) ;
#21265=VERTEX_POINT ( 'NONE', #2473 ) ;
#21284=CARTESIAN_POINT ( 'NONE',  ( -57.68749999999996447, 0.7533615035078072841, -3.673546848079177085 ) ) ;
#21287=CARTESIAN_POINT ( 'NONE',  ( -58.37486116251334067, -1.737685414808511020, 3.471684241605569099 ) ) ;
#21298=ORIENTED_EDGE ( 'NONE', *, *, #15150, .T. ) ;
#21300=FACE_OUTER_BOUND ( 'NONE', #30220, .T. ) ;
#21308=EDGE_LOOP ( 'NONE', ( #25688, #11288 ) ) ;
#21320=CARTESIAN_POINT ( 'NONE',  ( -58.68749999999997158, -4.108500314926509134, 1.367561758111400128 ) ) ;
#21341=CARTESIAN_POINT ( 'NONE',  ( -55.48542740578360366, -3.725040285533364859, 1.239922660687674760 ) ) ;
#21352=CYLINDRICAL_SURFACE ( 'NONE', #23153, 2.100000000000000089 ) ;
#21363=CARTESIAN_POINT ( 'NONE',  ( -56.53335481156723574, 0.7533615035078095046, -3.673546848079178861 ) ) ;
#21364=CARTESIAN_POINT ( 'NONE',  ( -58.04792740578360366, 3.330682475591786318, 0.6830477631804268146 ) ) ;
#21386=CARTESIAN_POINT ( 'NONE',  ( -60.23542740578359656, 2.936324665650206889, 2.606018187048499524 ) ) ;
#21389=( BOUNDED_CURVE ( )  B_SPLINE_CURVE ( 2, ( #6120, #20386, #30174, #30009, #3892, #8490, #11026, #1654, #8779 ),
 .UNSPECIFIED., .F., .T. ) 
 B_SPLINE_CURVE_WITH_KNOTS ( ( 3, 2, 2, 2, 3 ),
 ( 0.6944444444444445308, 0.7037037037037037202, 0.7222222222222222099, 0.7407407407407406996, 0.7500000000000000000 ),
 .UNSPECIFIED. ) 
 CURVE ( )  GEOMETRIC_REPRESENTATION_ITEM ( )  RATIONAL_B_SPLINE_CURVE ( ( 0.9330127018922194093, 0.9330127018922197424, 1.000000000000000000, 0.8660254037844387076, 1.000000000000000000, 0.8660254037844387076, 1.000000000000000000, 0.9330127018922194093, 0.9330127018922194093 ) ) 
 REPRESENTATION_ITEM ( '' )  );
#21390=CARTESIAN_POINT ( 'NONE',  ( -59.18749999999996447, 0.7533615035078157218, -3.673546848079175309 ) ) ;
#21394=CARTESIAN_POINT ( 'NONE',  ( -57.06249999999997158, -3.238593381231830381, -2.874284765127031793 ) ) ;
#21400=CARTESIAN_POINT ( 'NONE',  ( -55.28335481156723574, -4.108500314926509134, 1.367561758111407011 ) ) ;
#21409=DIRECTION ( 'NONE',  ( -1.000000000000000000, -3.054025858079668409E-16, 2.042474015755241579E-16 ) ) ;
#21422=ORIENTED_EDGE ( 'NONE', *, *, #16478, .F. ) ;
#21449=AXIS2_PLACEMENT_3D ( 'NONE', #28034, #3978, #20930 ) ;
#21459=DIRECTION ( 'NONE',  ( 0.000000000000000000, 0.2008964009354147762, -0.9796124928211139560 ) ) ;
#21465=DIRECTION ( 'NONE',  ( 0.000000000000000000, -0.2008964009354147484, 0.9796124928211139560 ) ) ;
#21467=CARTESIAN_POINT ( 'NONE',  ( -71.49999999999998579, -0.4218824419643727452, 2.057186234924342827 ) ) ;
#21478=CARTESIAN_POINT ( 'NONE',  ( -55.81249999999997868, -0.7533615035078013999, 3.673546848079176641 ) ) ;
#21487=CARTESIAN_POINT ( 'NONE',  ( -60.84585481156722864, 3.673546848079181970, 0.7533615035078072841 ) ) ;
#21533=CARTESIAN_POINT ( 'NONE',  ( -55.24999999999997868, 3.673546848079180638, 0.7533615035078055078 ) ) ;
#21542=EDGE_CURVE ( 'NONE', #29879, #29844, #22950, .T. ) ;
#21544=TOROIDAL_SURFACE ( 'NONE', #22633, 2.150000000000000355, 0.05000000000000000278 ) ;
#21547=CARTESIAN_POINT ( 'NONE',  ( -57.24999999999996447, -2.489203624310589280, 2.804704140674913138 ) ) ;
#21553=EDGE_CURVE ( 'NONE', #5904, #10453, #30562, .T. ) ;
#21577=ORIENTED_EDGE ( 'NONE', *, *, #15945, .T. ) ;
#21625=EDGE_CURVE ( 'NONE', #19589, #26980, #27189, .T. ) ;
#21635=FACE_OUTER_BOUND ( 'NONE', #30604, .T. ) ;
#21657=ORIENTED_EDGE ( 'NONE', *, *, #22376, .T. ) ;
#21659=CARTESIAN_POINT ( 'NONE',  ( -56.48542740578359656, 2.936324665650207333, 2.606018187048499080 ) ) ;
#21666=AXIS2_PLACEMENT_3D ( 'NONE', #30703, #25632, #15680 ) ;
#21676=DIRECTION ( 'NONE',  ( 1.000000000000000000, 3.054025858079668409E-16, -2.042474015755241579E-16 ) ) ;
#21703=CARTESIAN_POINT ( 'NONE',  ( -59.98542740578359656, -3.725040285533365303, 1.239922660687675871 ) ) ;
#21704=DIRECTION ( 'NONE',  ( 2.581436205204234006E-16, -0.9796124928211140670, -0.2008964009354148872 ) ) ;
#21730=CARTESIAN_POINT ( 'NONE',  ( -59.29999999999997584, 3.111192537532289304, 2.093557019620777115 ) ) ;
#21735=CARTESIAN_POINT ( 'NONE',  ( -57.62486116251334778, -1.737685414808515683, 3.471684241605564658 ) ) ;
#21741=CARTESIAN_POINT ( 'NONE',  ( -57.72499999999997300, -0.9643027244899882167, 4.702139965541347166 ) ) ;
#21763=DIRECTION ( 'NONE',  ( 0.000000000000000000, -0.2008964009354147484, 0.9796124928211139560 ) ) ;
#21771=CARTESIAN_POINT ( 'NONE',  ( -58.99999999999997158, 3.673546848079179306, 0.7533615035078117250 ) ) ;
#21774=CARTESIAN_POINT ( 'NONE',  ( -58.40835481156723574, -0.7533615035077920741, 3.673546848079180638 ) ) ;
#21776=ORIENTED_EDGE ( 'NONE', *, *, #5613, .T. ) ;
#21785=EDGE_CURVE ( 'NONE', #5904, #6063, #2234, .T. ) ;
#21809=CARTESIAN_POINT ( 'NONE',  ( -60.09585481156723574, 3.673546848079181970, 0.7533615035078071731 ) ) ;
#21856=ORIENTED_EDGE ( 'NONE', *, *, #13505, .F. ) ;
#21857=CARTESIAN_POINT ( 'NONE',  ( -59.74999999999997158, 3.673546848079180194, 0.7533615035078065070 ) ) ;
#21870=FACE_OUTER_BOUND ( 'NONE', #28848, .T. ) ;
#21880=CARTESIAN_POINT ( 'NONE',  ( -59.19184846062112371, 0.2309624077929078034, 3.875409454552792621 ) ) ;
#21910=CIRCLE ( 'NONE', #29458, 2.050000000000000266 ) ;
#21947=DIRECTION ( 'NONE',  ( 1.000000000000000000, 3.054025858079668409E-16, -2.042474015755241579E-16 ) ) ;
#21949=EDGE_CURVE ( 'NONE', #29844, #29879, #29050, .T. ) ;
#21954=CARTESIAN_POINT ( 'NONE',  ( -54.29792740578361077, 3.330682475591790315, 0.6830477631804100502 ) ) ;
#21981=EDGE_LOOP ( 'NONE', ( #13760, #5933, #30088, #18374 ) ) ;
#21995=ORIENTED_EDGE ( 'NONE', *, *, #23186, .F. ) ;
#21996=CARTESIAN_POINT ( 'NONE',  ( -60.93749999999995737, -4.108500314926507357, 1.367561758111407455 ) ) ;
#21998=DIRECTION ( 'NONE',  ( 1.000000000000000000, 3.054025858079668409E-16, -2.042474015755241579E-16 ) ) ;
#22001=CARTESIAN_POINT ( 'NONE',  ( -55.02900635094608361, -1.737685414808514794, 3.471684241605561994 ) ) ;
#22014=DIRECTION ( 'NONE',  ( 1.000000000000000000, 3.054025858079668409E-16, -2.042474015755241579E-16 ) ) ;
#22015=LINE ( 'NONE', #10275, #20047 ) ;
#22034=CARTESIAN_POINT ( 'NONE',  ( -55.04792740578361077, 3.330682475591790315, 0.6830477631804101613 ) ) ;
#22053=AXIS2_PLACEMENT_3D ( 'NONE', #22599, #5971, #15626 ) ;
#22059=EDGE_LOOP ( 'NONE', ( #3539, #22743 ) ) ;
#22068=DIRECTION ( 'NONE',  ( 2.581436205204234499E-16, -0.9796124928211140670, -0.2008964009354146651 ) ) ;
#22085=AXIS2_PLACEMENT_3D ( 'NONE', #23519, #16395, #14006 ) ;
#22113=DIRECTION ( 'NONE',  ( 1.000000000000000000, 3.054025858079668409E-16, -2.042474015755241579E-16 ) ) ;
#22114=CARTESIAN_POINT ( 'NONE',  ( -57.61042740578359656, -2.936324665650201116, -2.606018187048497747 ) ) ;
#22160=CARTESIAN_POINT ( 'NONE',  ( -60.56249999999997158, 4.108500314926511798, -1.367561758111406345 ) ) ;
#22162=CARTESIAN_POINT ( 'NONE',  ( -55.18749999999997158, 3.238593381231846369, 2.874284765127020691 ) ) ;
#22175=CARTESIAN_POINT ( 'NONE',  ( -56.59599364905386665, 0.2309624077929022246, 3.875409454552789956 ) ) ;
#22232=ORIENTED_EDGE ( 'NONE', *, *, #30713, .T. ) ;
#22259=TOROIDAL_SURFACE ( 'NONE', #13119, 4.800000000000000711, 0.05000000000000000278 ) ;
#22266=CARTESIAN_POINT ( 'NONE',  ( -58.04792740578360366, 3.330682475591789427, 0.6830477631804109384 ) ) ;
#22267=CARTESIAN_POINT ( 'NONE',  ( -59.29999999999997584, 2.330309927981285032E-15, 4.253626757584724400E-16 ) ) ;
#22279=FACE_BOUND ( 'NONE', #20323, .T. ) ;
#22297=ORIENTED_EDGE ( 'NONE', *, *, #19474, .F. ) ;
#22312=CARTESIAN_POINT ( 'NONE',  ( -60.37499999999996447, 1.184343223768589803, 3.558065644182725862 ) ) ;
#22320=EDGE_CURVE ( 'NONE', #28519, #24531, #26537, .T. ) ;
#22376=EDGE_CURVE ( 'NONE', #6162, #25369, #8312, .T. ) ;
#22392=LINE ( 'NONE', #29490, #5139 ) ;
#22402=EDGE_CURVE ( 'NONE', #24313, #9750, #30564, .T. ) ;
#22409=CARTESIAN_POINT ( 'NONE',  ( -60.29792740578359656, 3.330682475591789427, 0.6830477631804114935 ) ) ;
#22414=CARTESIAN_POINT ( 'NONE',  ( -67.97846802697301882, -3.201166483080443511E-16, 2.197917219923980763E-15 ) ) ;
#22437=CARTESIAN_POINT ( 'NONE',  ( -59.29999999999997584, 0.05651759653475140616, 3.560132860530125232 ) ) ;
#22445=CARTESIAN_POINT ( 'NONE',  ( -54.09585481156724285, 3.673546848079182858, 0.7533615035078057298 ) ) ;
#22458=CARTESIAN_POINT ( 'NONE',  ( -57.87499999999997158, -3.673546848079173976, -0.7533615035078061739 ) ) ;
#22483=ORIENTED_EDGE ( 'NONE', *, *, #19889, .T. ) ;
#22485=EDGE_CURVE ( 'NONE', #9864, #18872, #2153, .T. ) ;
#22490=CARTESIAN_POINT ( 'NONE',  ( -54.42292740578361077, 2.256877952708269852, -2.542931754211926076 ) ) ;
#22515=DIRECTION ( 'NONE',  ( 0.000000000000000000, 0.2008964009354147484, -0.9796124928211139560 ) ) ;
#22528=DIRECTION ( 'NONE',  ( 0.000000000000000000, 0.2008964009354143876, -0.9796124928211140670 ) ) ;
#22548=CARTESIAN_POINT ( 'NONE',  ( -59.29999999999997584, 0.7533615035078071731, -3.673546848079177529 ) ) ;
#22562=EDGE_LOOP ( 'NONE', ( #19817, #1971, #18637, #20862 ) ) ;
#22568=CARTESIAN_POINT ( 'NONE',  ( -57.86042740578360366, -0.7887156198831604126, 3.845940847736174284 ) ) ;
#22597=ADVANCED_FACE ( 'NONE', ( #24324 ), #28545, .T. ) ;
#22599=CARTESIAN_POINT ( 'NONE',  ( -57.72499999999997300, 2.811319000628834039E-15, 1.036730182770210180E-16 ) ) ;
#22607=ORIENTED_EDGE ( 'NONE', *, *, #1113, .F. ) ;
#22618=ADVANCED_FACE ( 'NONE', ( #25082 ), #9345, .T. ) ;
#22626=CARTESIAN_POINT ( 'NONE',  ( -59.29999999999997584, 0.7533615035078071731, -3.673546848079177529 ) ) ;
#22630=CARTESIAN_POINT ( 'NONE',  ( -59.29999999999997584, 2.330309927981285032E-15, 4.253626757584724400E-16 ) ) ;
#22633=AXIS2_PLACEMENT_3D ( 'NONE', #6653, #6334, #4438 ) ;
#22642=EDGE_CURVE ( 'NONE', #5992, #9864, #2314, .T. ) ;
#22645=CARTESIAN_POINT ( 'NONE',  ( -54.52560264074444518, -0.4085193297958337744, -3.447427373925056493 ) ) ;
#22662=CARTESIAN_POINT ( 'NONE',  ( -59.15835481156722864, -0.7533615035078041755, 3.673546848079178861 ) ) ;
#22666=CARTESIAN_POINT ( 'NONE',  ( -58.36042740578360366, -2.936324665650201116, -2.606018187048497747 ) ) ;
#22679=EDGE_CURVE ( 'NONE', #2190, #25428, #10863, .T. ) ;
#22699=ORIENTED_EDGE ( 'NONE', *, *, #26897, .F. ) ;
#22705=ORIENTED_EDGE ( 'NONE', *, *, #7003, .F. ) ;
#22714=CIRCLE ( 'NONE', #1459, 3.598079936076698182 ) ;
#22728=ORIENTED_EDGE ( 'NONE', *, *, #9373, .T. ) ;
#22735=CARTESIAN_POINT ( 'NONE',  ( -58.48542740578359656, -3.725040285533365303, 1.239922660687675648 ) ) ;
#22741=ORIENTED_EDGE ( 'NONE', *, *, #21553, .F. ) ;
#22743=ORIENTED_EDGE ( 'NONE', *, *, #6112, .F. ) ;
#22752=CARTESIAN_POINT ( 'NONE',  ( -54.54999999999998295, 0.9743475445367651977, -4.751120590182403625 ) ) ;
#22754=EDGE_CURVE ( 'NONE', #2983, #333, #10371, .T. ) ;
#22768=ORIENTED_EDGE ( 'NONE', *, *, #25943, .T. ) ;
#22774=CARTESIAN_POINT ( 'NONE',  ( -54.40835481156724285, -3.238593381231841928, -2.874284765127022911 ) ) ;
#22789=ADVANCED_FACE ( 'NONE', ( #8615 ), #23494, .F. ) ;
#22820=CARTESIAN_POINT ( 'NONE',  ( -58.42292740578360366, -3.330682475591783653, -0.6830477631804107164 ) ) ;
#22826=AXIS2_PLACEMENT_3D ( 'NONE', #3639, #27392, #29922 ) ;
#22862=VERTEX_POINT ( 'NONE', #4968 ) ;
#22871=DIRECTION ( 'NONE',  ( 2.614381936396368743E-16, -0.2008964009354147762, 0.9796124928211139560 ) ) ;
#22895=DIRECTION ( 'NONE',  ( -2.614381936396368743E-16, 0.2008964009354147762, -0.9796124928211139560 ) ) ;
#22898=CARTESIAN_POINT ( 'NONE',  ( -57.84585481156723574, 3.673546848079182414, 0.7533615035078065070 ) ) ;
#22916=CARTESIAN_POINT ( 'NONE',  ( -54.15835481156724285, 4.108500314926515351, -1.367561758111409009 ) ) ;
#22924=ORIENTED_EDGE ( 'NONE', *, *, #3615, .T. ) ;
#22943=EDGE_CURVE ( 'NONE', #13554, #236, #31100, .T. ) ;
#22950=CIRCLE ( 'NONE', #21449, 3.075000000000000622 ) ;
#22960=CARTESIAN_POINT ( 'NONE',  ( -55.79792740578360366, 3.330682475591789871, 0.6830477631804102723 ) ) ;
#22961=EDGE_CURVE ( 'NONE', #24734, #27277, #3788, .T. ) ;
#22981=CARTESIAN_POINT ( 'NONE',  ( -54.49999999999997158, 1.284124781083705313, -3.226451220649914742 ) ) ;
#23011=DIRECTION ( 'NONE',  ( -1.000000000000000000, -3.054025858079668409E-16, 2.042474015755241579E-16 ) ) ;
#23024=EDGE_CURVE ( 'NONE', #9046, #11104, #9368, .T. ) ;
#23026=EDGE_LOOP ( 'NONE', ( #13818, #29231, #18873, #27969 ) ) ;
#23037=DIRECTION ( 'NONE',  ( 0.000000000000000000, -0.2008964009354147484, 0.9796124928211139560 ) ) ;
#23046=CIRCLE ( 'NONE', #15440, 2.114644660940672605 ) ;
#23053=DIRECTION ( 'NONE',  ( 0.000000000000000000, 0.2008964009354147484, -0.9796124928211138450 ) ) ;
#23065=CARTESIAN_POINT ( 'NONE',  ( -58.81249999999996447, -0.7533615035078081723, 3.673546848079176197 ) ) ;
#23073=CARTESIAN_POINT ( 'NONE',  ( -58.47085481156723574, 1.184343223768590692, 3.558065644182727194 ) ) ;
#23085=CARTESIAN_POINT ( 'NONE',  ( -67.99999999999995737, -3.266925685480207642E-16, 2.202315069465528948E-15 ) ) ;
#23101=CARTESIAN_POINT ( 'NONE',  ( -55.11042740578361077, 3.725040285533371964, -1.239922660687673650 ) ) ;
#23102=ADVANCED_FACE ( 'NONE', ( #25511 ), #30268, .T. ) ;
#23106=CARTESIAN_POINT ( 'NONE',  ( -59.29999999999997584, 2.330309927981285032E-15, 4.253626757584724400E-16 ) ) ;
#23127=CARTESIAN_POINT ( 'NONE',  ( -57.42292740578360366, 2.256877952708269408, -2.542931754211925188 ) ) ;
#23139=FACE_OUTER_BOUND ( 'NONE', #17423, .T. ) ;
#23149=CARTESIAN_POINT ( 'NONE',  ( -54.49999999999997868, 3.433573722926734462, -1.225502693192425774 ) ) ;
#23153=AXIS2_PLACEMENT_3D ( 'NONE', #16113, #25762, #30979 ) ;
#23184=FACE_OUTER_BOUND ( 'NONE', #26958, .T. ) ;
#23186=EDGE_CURVE ( 'NONE', #9168, #18443, #8574, .T. ) ;
#23192=CARTESIAN_POINT ( 'NONE',  ( -59.29999999999997584, 3.111192537532289304, 2.093557019620777115 ) ) ;
#23194=CARTESIAN_POINT ( 'NONE',  ( -67.98046642889043767, -3.207269654211098678E-16, 2.198325388322918801E-15 ) ) ;
#23214=CARTESIAN_POINT ( 'NONE',  ( -54.78335481156722864, 3.238593381231848145, 2.874284765127022023 ) ) ;
#23231=VERTEX_POINT ( 'NONE', #26573 ) ;
#23233=CARTESIAN_POINT ( 'NONE',  ( -56.90835481156723574, -0.8699069336946628761, 4.241846523238430144 ) ) ;
#23257=CARTESIAN_POINT ( 'NONE',  ( -59.04792740578360366, -1.073804522883505363, -3.225979517392338902 ) ) ;
#23277=CARTESIAN_POINT ( 'NONE',  ( -55.78335481156724285, 0.7533615035078067290, -3.673546848079180194 ) ) ;
#23279=CARTESIAN_POINT ( 'NONE',  ( -58.67292740578360366, 1.073804522883521351, 3.225979517392336682 ) ) ;
#23282=EDGE_CURVE ( 'NONE', #16493, #31001, #10735, .T. ) ;
#23284=AXIS2_PLACEMENT_3D ( 'NONE', #30615, #30314, #21158 ) ;
#23291=LINE ( 'NONE', #23766, #8375 ) ;
#23330=CARTESIAN_POINT ( 'NONE',  ( -71.44781903063172024, 0.2962147058074188766, -1.444404304980887455 ) ) ;
#23353=CARTESIAN_POINT ( 'NONE',  ( -61.12499999999996447, 1.184343223768589803, 3.558065644182725862 ) ) ;
#23383=CARTESIAN_POINT ( 'NONE',  ( -55.65835481156724285, 4.108500314926515351, -1.367561758111408343 ) ) ;
#23387=ORIENTED_EDGE ( 'NONE', *, *, #23526, .T. ) ;
#23390=DIRECTION ( 'NONE',  ( -1.000000000000000000, -3.054025858079668409E-16, 2.042474015755241579E-16 ) ) ;
#23406=CARTESIAN_POINT ( 'NONE',  ( -59.29999999999997584, -2.208048483361063852, 2.585444235547710967 ) ) ;
#23417=EDGE_LOOP ( 'NONE', ( #2848, #2701, #11144, #16913 ) ) ;
#23427=ORIENTED_EDGE ( 'NONE', *, *, #7889, .F. ) ;
#23428=CARTESIAN_POINT ( 'NONE',  ( -60.48542740578360366, 0.7887156198831658527, -3.845940847736173840 ) ) ;
#23429=VECTOR ( 'NONE', #18672, 1000.000000000000114 ) ;
#23433=CARTESIAN_POINT ( 'NONE',  ( -67.99999999999997158, -3.266925685480240183E-16, 2.202315069465531314E-15 ) ) ;
#23436=CARTESIAN_POINT ( 'NONE',  ( -57.12499999999997158, -3.673546848079173532, -0.7533615035078090605 ) ) ;
#23481=FACE_OUTER_BOUND ( 'NONE', #28447, .T. ) ;
#23488=ORIENTED_EDGE ( 'NONE', *, *, #17984, .T. ) ;
#23494=CYLINDRICAL_SURFACE ( 'NONE', #20497, 3.750000000000000444 ) ;
#23519=CARTESIAN_POINT ( 'NONE',  ( -67.99999999999995737, -3.266925685480207642E-16, 2.202315069465528948E-15 ) ) ;
#23526=EDGE_CURVE ( 'NONE', #25236, #9362, #12783, .T. ) ;
#23528=ORIENTED_EDGE ( 'NONE', *, *, #22485, .F. ) ;
#23532=ORIENTED_EDGE ( 'NONE', *, *, #13244, .F. ) ;
#23534=CARTESIAN_POINT ( 'NONE',  ( -58.78335481156723574, 0.8699069336946689823, -4.241846523238430144 ) ) ;
#23561=AXIS2_PLACEMENT_3D ( 'NONE', #27950, #1653, #28273 ) ;
#23563=CARTESIAN_POINT ( 'NONE',  ( -56.04792740578360366, -1.073804522883513579, -3.225979517392337126 ) ) ;
#23588=CARTESIAN_POINT ( 'NONE',  ( -60.67292740578359656, -3.330682475591783653, -0.6830477631804101613 ) ) ;
#23600=CARTESIAN_POINT ( 'NONE',  ( -69.18535533905931345, 0.4248245016402701912, -2.071532327734947110 ) ) ;
#23618=CONICAL_SURFACE ( 'NONE', #27149, 2.099999999999999645, 0.7853981633974396193 ) ;
#23632=DIRECTION ( 'NONE',  ( 1.000000000000000000, 3.054025858079668409E-16, -2.042474015755241579E-16 ) ) ;
#23637=VECTOR ( 'NONE', #10785, 1000.000000000000114 ) ;
#23665=DIRECTION ( 'NONE',  ( 0.000000000000000000, 0.2008964009354148039, -0.9796124928211140670 ) ) ;
#23684=EDGE_LOOP ( 'NONE', ( #27076, #22483 ) ) ;
#23690=CARTESIAN_POINT ( 'NONE',  ( -54.84585481156724285, 3.673546848079182858, 0.7533615035078058408 ) ) ;
#23694=DIRECTION ( 'NONE',  ( 1.000000000000000000, 3.054027077731387480E-16, -2.042479963029832083E-16 ) ) ;
#23707=CARTESIAN_POINT ( 'NONE',  ( -57.59585481156722864, -2.489203624310587060, 2.804704140674918467 ) ) ;
#23713=ORIENTED_EDGE ( 'NONE', *, *, #22485, .T. ) ;
#23727=DIRECTION ( 'NONE',  ( 0.000000000000000000, -0.2008964009354147484, 0.9796124928211139560 ) ) ;
#23729=CARTESIAN_POINT ( 'NONE',  ( -57.67292740578359656, -3.330682475591780101, -0.6830477631804258154 ) ) ;
#23730=ADVANCED_FACE ( 'NONE', ( #8336 ), #16935, .T. ) ;
#23751=CARTESIAN_POINT ( 'NONE',  ( -60.04792740578359656, -2.256877952708263635, 2.542931754211925188 ) ) ;
#23753=CARTESIAN_POINT ( 'NONE',  ( -54.59585481156724285, -2.489203624310586616, 2.804704140674918023 ) ) ;
#23766=CARTESIAN_POINT ( 'NONE',  ( -59.29999999999997584, 0.7533615035078071731, -3.673546848079177529 ) ) ;
#23780=EDGE_CURVE ( 'NONE', #12772, #5904, #10759, .T. ) ;
#23791=ORIENTED_EDGE ( 'NONE', *, *, #2864, .F. ) ;
#23824=ORIENTED_EDGE ( 'NONE', *, *, #22943, .F. ) ;
#23849=EDGE_LOOP ( 'NONE', ( #13635, #29001, #17784 ) ) ;
#23856=CARTESIAN_POINT ( 'NONE',  ( -56.23542740578360366, -3.725040285533364859, 1.239922660687674982 ) ) ;
#23857=DIRECTION ( 'NONE',  ( 0.000000000000000000, 0.2008964009354147762, -0.9796124928211140670 ) ) ;
#23870=EDGE_CURVE ( 'NONE', #25369, #16804, #21910, .T. ) ;
#23880=CARTESIAN_POINT ( 'NONE',  ( -56.67292740578360366, 2.256877952708273849, -2.542931754211921191 ) ) ;
#23899=CARTESIAN_POINT ( 'NONE',  ( -59.79792740578359656, -1.073804522883517576, -3.225979517392334905 ) ) ;
#23905=CARTESIAN_POINT ( 'NONE',  ( -56.67499999999996874, -0.9743475445367589804, 4.751120590182402736 ) ) ;
#23909=DIRECTION ( 'NONE',  ( 0.000000000000000000, 0.2008964009354148039, -0.9796124928211140670 ) ) ;
#23920=ORIENTED_EDGE ( 'NONE', *, *, #21542, .F. ) ;
#23930=ORIENTED_EDGE ( 'NONE', *, *, #11947, .F. ) ;
#23943=VERTEX_POINT ( 'NONE', #9870 ) ;
#23945=CARTESIAN_POINT ( 'NONE',  ( -57.65400635094607651, 1.737685414808524342, -3.471684241605563770 ) ) ;
#23960=CARTESIAN_POINT ( 'NONE',  ( -54.49999999999997868, -3.745083032500879039, 0.1919715595446555012 ) ) ;
#23979=VERTEX_POINT ( 'NONE', #8116 ) ;
#24004=CARTESIAN_POINT ( 'NONE',  ( -55.67292740578360366, 1.073804522883522239, 3.225979517392336238 ) ) ;
#24014=AXIS2_PLACEMENT_3D ( 'NONE', #11039, #1209, #4063 ) ;
#24047=CARTESIAN_POINT ( 'NONE',  ( -55.12499999999997868, 1.184343223768590692, 3.558065644182724530 ) ) ;
#24049=CARTESIAN_POINT ( 'NONE',  ( -54.62486116251335488, -1.737685414808515239, 3.471684241605564214 ) ) ;
#24063=LINE ( 'NONE', #26437, #24730 ) ;
#24098=EDGE_LOOP ( 'NONE', ( #24393, #29807, #23387, #14330 ) ) ;
#24102=LINE ( 'NONE', #26927, #7485 ) ;
#24106=CONICAL_SURFACE ( 'NONE', #22085, 3.299999999999999822, 0.03997868712329010615 ) ;
#24148=DIRECTION ( 'NONE',  ( 0.000000000000000000, 0.2008964009354148594, -0.9796124928211140670 ) ) ;
#24151=CARTESIAN_POINT ( 'NONE',  ( -71.49999999999998579, -0.4118376219176019259, 2.008205610283286813 ) ) ;
#24168=CARTESIAN_POINT ( 'NONE',  ( -59.84585481156722864, -2.489203624310587504, 2.804704140674918911 ) ) ;
#24215=CARTESIAN_POINT ( 'NONE',  ( -58.87499999999997158, 1.184343223768590025, 3.558065644182725418 ) ) ;
#24233=( GEOMETRIC_REPRESENTATION_CONTEXT ( 3 ) GLOBAL_UNCERTAINTY_ASSIGNED_CONTEXT ( ( #19343 ) ) GLOBAL_UNIT_ASSIGNED_CONTEXT ( ( #24746, #15243, #7968 ) ) REPRESENTATION_CONTEXT ( 'NONE', 'WORKASPACE' ) );
#24245=CARTESIAN_POINT ( 'NONE',  ( -57.47085481156722864, -3.673546848079175753, -0.7533615035078066180 ) ) ;
#24256=ORIENTED_EDGE ( 'NONE', *, *, #29700, .T. ) ;
#24265=CARTESIAN_POINT ( 'NONE',  ( -71.49999999999998579, 0.3062499654112549874, -1.493338310920502066 ) ) ;
#24266=VECTOR ( 'NONE', #4691, 1000.000000000000000 ) ;
#24289=EDGE_LOOP ( 'NONE', ( #28485, #25897, #19543, #526 ) ) ;
#24308=CIRCLE ( 'NONE', #9657, 1.625000000000000444 ) ;
#24313=VERTEX_POINT ( 'NONE', #19204 ) ;
#24314=EDGE_CURVE ( 'NONE', #24734, #11521, #1758, .T. ) ;
#24318=CARTESIAN_POINT ( 'NONE',  ( -54.54792740578361077, -1.073804522883516688, -3.225979517392336238 ) ) ;
#24324=FACE_OUTER_BOUND ( 'NONE', #12004, .T. ) ;
#24327=EDGE_LOOP ( 'NONE', ( #22768, #28292, #15209, #31033 ) ) ;
#24354=EDGE_CURVE ( 'NONE', #26583, #14688, #4154, .T. ) ;
#24362=CARTESIAN_POINT ( 'NONE',  ( -57.68749999999996447, 0.8699069336946685382, -4.241846523238428368 ) ) ;
#24367=CARTESIAN_POINT ( 'NONE',  ( -54.68749999999997868, 0.7533615035078081723, -3.673546848079177973 ) ) ;
#24369=DIRECTION ( 'NONE',  ( -2.614381936396368743E-16, 0.2008964009354147762, -0.9796124928211139560 ) ) ;
#24392=CARTESIAN_POINT ( 'NONE',  ( -57.31684846062113792, -0.2309624077929026409, -3.875409454552791733 ) ) ;
#24393=ORIENTED_EDGE ( 'NONE', *, *, #28816, .F. ) ;
#24408=ADVANCED_FACE ( 'NONE', ( #27391 ), #12874, .T. ) ;
#24449=DIRECTION ( 'NONE',  ( 0.000000000000000000, -0.2008964009354147484, 0.9796124928211139560 ) ) ;
#24454=EDGE_LOOP ( 'NONE', ( #15888, #19252, #14664, #4032 ) ) ;
#24455=ADVANCED_FACE ( 'NONE', ( #9832 ), #18151, .T. ) ;
#24458=CARTESIAN_POINT ( 'NONE',  ( -56.36042740578360366, -0.7887156198831599685, 3.845940847736173840 ) ) ;
#24468=( BOUNDED_CURVE ( )  B_SPLINE_CURVE ( 2, ( #26886, #2816, #12471, #22162, #450, #19780, #27032, #5342, #24673 ),
 .UNSPECIFIED., .F., .T. ) 
 B_SPLINE_CURVE_WITH_KNOTS ( ( 3, 2, 2, 2, 3 ),
 ( 0.08333333333333332871, 0.09259259259259258745, 0.1111111111111111049, 0.1296296296296296224, 0.1388888888888888951 ),
 .UNSPECIFIED. ) 
 CURVE ( )  GEOMETRIC_REPRESENTATION_ITEM ( )  RATIONAL_B_SPLINE_CURVE ( ( 0.9330127018922194093, 0.9330127018922194093, 1.000000000000000000, 0.8660254037844387076, 1.000000000000000000, 0.8660254037844387076, 1.000000000000000000, 0.9330127018922191873, 0.9330127018922192983 ) ) 
 REPRESENTATION_ITEM ( '' )  );
#24479=AXIS2_PLACEMENT_3D ( 'NONE', #11133, #3113, #1477 ) ;
#24483=EDGE_LOOP ( 'NONE', ( #12380, #17379, #21776, #19493 ) ) ;
#24488=EDGE_CURVE ( 'NONE', #28519, #1074, #20527, .T. ) ;
#24489=FACE_OUTER_BOUND ( 'NONE', #7437, .T. ) ;
#24492=AXIS2_PLACEMENT_3D ( 'NONE', #8504, #20863, #25907 ) ;
#24502=CARTESIAN_POINT ( 'NONE',  ( -58.81249999999996447, -0.8699069336946627651, 4.241846523238428368 ) ) ;
#24511=ORIENTED_EDGE ( 'NONE', *, *, #10653, .T. ) ;
#24519=AXIS2_PLACEMENT_3D ( 'NONE', #4923, #9692, #2399 ) ;
#24531=VERTEX_POINT ( 'NONE', #929 ) ;
#24539=CARTESIAN_POINT ( 'NONE',  ( -55.48542740578360366, -3.725040285533364859, 1.239922660687674760 ) ) ;
#24552=DIRECTION ( 'NONE',  ( -1.000000000000000000, -3.054025858079668409E-16, 2.042474015755241579E-16 ) ) ;
#24553=DIRECTION ( 'NONE',  ( -1.000000000000000000, -3.054025858079668409E-16, 2.042474015755241579E-16 ) ) ;
#24556=CARTESIAN_POINT ( 'NONE',  ( -67.99999999999997158, 0.3264566515200485464, -1.591870300834308471 ) ) ;
#24561=DIRECTION ( 'NONE',  ( 1.000000000000000000, 3.054025858079668409E-16, -2.042474015755241579E-16 ) ) ;
#24577=ADVANCED_FACE ( 'NONE', ( #28256 ), #10889, .T. ) ;
#24588=CARTESIAN_POINT ( 'NONE',  ( -71.44999999999998863, -0.4218824419643722456, 2.057186234924342383 ) ) ;
#24594=( BOUNDED_CURVE ( )  B_SPLINE_CURVE ( 2, ( #24367, #19933, #3296, #26888, #29115, #7432, #3140, #22001, #27207 ),
 .UNSPECIFIED., .F., .T. ) 
 B_SPLINE_CURVE_WITH_KNOTS ( ( 3, 2, 2, 2, 3 ),
 ( 0.02777777777777778317, 0.03703703703703703498, 0.05555555555555555247, 0.07407407407407406996, 0.08333333333333332871 ),
 .UNSPECIFIED. ) 
 CURVE ( )  GEOMETRIC_REPRESENTATION_ITEM ( )  RATIONAL_B_SPLINE_CURVE ( ( 0.9330127018922194093, 0.9330127018922194093, 1.000000000000000000, 0.8660254037844387076, 1.000000000000000000, 0.8660254037844387076, 1.000000000000000000, 0.9330127018922194093, 0.9330127018922194093 ) ) 
 REPRESENTATION_ITEM ( '' )  );
#24618=CARTESIAN_POINT ( 'NONE',  ( -60.48542740578360366, 0.7887156198831658527, -3.845940847736173840 ) ) ;
#24630=CARTESIAN_POINT ( 'NONE',  ( -58.18749999999997158, 3.238593381231836155, 2.874284765127033126 ) ) ;
#24667=ORIENTED_EDGE ( 'NONE', *, *, #23870, .F. ) ;
#24671=CARTESIAN_POINT ( 'NONE',  ( -57.31249999999996447, -0.8699069336946624320, 4.241846523238428368 ) ) ;
#24673=CARTESIAN_POINT ( 'NONE',  ( -55.43749999999997868, 0.7533615035078096156, -3.673546848079177529 ) ) ;
#24686=CARTESIAN_POINT ( 'NONE',  ( -56.93749999999996447, 0.7533615035078061739, -3.673546848079177973 ) ) ;
#24689=VERTEX_POINT ( 'NONE', #9696 ) ;
#24692=UNCERTAINTY_MEASURE_WITH_UNIT (LENGTH_MEASURE( 1.000000000000000082E-05 ), #5866, 'distance_accuracy_value', 'NONE');
#24704=EDGE_CURVE ( 'NONE', #27277, #18051, #2801, .T. ) ;
#24705=CARTESIAN_POINT ( 'NONE',  ( -54.54999999999998295, 3.780972210569126836E-15, -5.448124817252668230E-16 ) ) ;
#24721=EDGE_CURVE ( 'NONE', #9227, #19802, #13738, .T. ) ;
#24730=VECTOR ( 'NONE', #4730, 1000.000000000000000 ) ;
#24734=VERTEX_POINT ( 'NONE', #12350 ) ;
#24746=( LENGTH_UNIT ( ) NAMED_UNIT ( * ) SI_UNIT ( .MILLI., .METRE. ) );
#24765=CIRCLE ( 'NONE', #11112, 3.075000000000000622 ) ;
#24775=CARTESIAN_POINT ( 'NONE',  ( -57.04792740578359656, -2.256877952708263635, 2.542931754211924300 ) ) ;
#24806=ORIENTED_EDGE ( 'NONE', *, *, #13244, .T. ) ;
#24822=CARTESIAN_POINT ( 'NONE',  ( -58.37499999999997158, 2.489203624310591056, -2.804704140674917578 ) ) ;
#24859=CARTESIAN_POINT ( 'NONE',  ( -71.44999999999998863, -1.380331489585512972E-15, 2.906968604901091669E-15 ) ) ;
#24873=ORIENTED_EDGE ( 'NONE', *, *, #16478, .T. ) ;
#24875=DIRECTION ( 'NONE',  ( 0.000000000000000000, -0.2008964009354147762, 0.9796124928211140670 ) ) ;
#24889=SURFACE_STYLE_FILL_AREA ( #20296 ) ;
#24903=CARTESIAN_POINT ( 'NONE',  ( -56.72499999999997300, 0.9643027244899941008, -4.702139965541347166 ) ) ;
#24912=DIRECTION ( 'NONE',  ( -1.000000000000000000, -3.054025858079668409E-16, 2.042474015755241579E-16 ) ) ;
#24918=AXIS2_PLACEMENT_3D ( 'NONE', #7672, #26977, #29054 ) ;
#24919=CARTESIAN_POINT ( 'NONE',  ( -56.92292740578359656, -3.330682475591783209, -0.6830477631804109384 ) ) ;
#24946=CARTESIAN_POINT ( 'NONE',  ( -59.29999999999994742, 1.055797642268307301, 3.459130888392116354 ) ) ;
#24951=CARTESIAN_POINT ( 'NONE',  ( -59.29999999999997584, 2.330309927981285032E-15, 4.253626757584724400E-16 ) ) ;
#24987=CARTESIAN_POINT ( 'NONE',  ( -67.97846802697301882, -3.201166483080443511E-16, 2.197917219923980763E-15 ) ) ;
#24988=AXIS2_PLACEMENT_3D ( 'NONE', #14848, #5055, #24369 ) ;
#24990=DIRECTION ( 'NONE',  ( 0.000000000000000000, -0.2008964009354147484, 0.9796124928211139560 ) ) ;
#25004=CARTESIAN_POINT ( 'NONE',  ( -59.29999999999998295, -2.594510663346734969, 2.255216637833513893 ) ) ;
#25014=EDGE_CURVE ( 'NONE', #18443, #15338, #24594, .T. ) ;
#25024=AXIS2_PLACEMENT_3D ( 'NONE', #12846, #19704, #22528 ) ;
#25028=CARTESIAN_POINT ( 'NONE',  ( -60.49999999999995737, 1.963826825011730345E-15, 6.704595576490977020E-16 ) ) ;
#25045=ORIENTED_EDGE ( 'NONE', *, *, #515, .F. ) ;
#25064=CARTESIAN_POINT ( 'NONE',  ( -55.43749999999997868, 0.7533615035078096156, -3.673546848079177529 ) ) ;
#25069=EDGE_CURVE ( 'NONE', #20313, #5081, #3560, .T. ) ;
#25076=CARTESIAN_POINT ( 'NONE',  ( -59.67292740578360366, 2.256877952708268964, -2.542931754211924744 ) ) ;
#25082=FACE_OUTER_BOUND ( 'NONE', #17407, .T. ) ;
#25109=CIRCLE ( 'NONE', #20618, 0.04999999999999989175 ) ;
#25129=CARTESIAN_POINT ( 'NONE',  ( -60.48535533905928219, 0.8667965836981847971, -4.226679811941398413 ) ) ;
#25140=CLOSED_SHELL ( 'NONE', ( #1556, #1055, #9161, #22597, #14720, #22618, #9748, #11125, #11113, #19949, #12388, #2451, #14939, #3259, #19236, #1009, #9141, #22789, #8612, #2019, #21072, #1184, #13953, #30247, #31309, #13373, #14590, #9982, #3483, #7597, #13253, #27402, #24577, #4000, #23102, #20147, #18701, #4233, #24455, #23730, #4005, #15054, #27037, #26098, #17979, #1661, #3071, #564, #15336, #25914, #8996, #1167, #13297, #1628, #30538, #3042, #8607, #15400, #27846, #24408, #4966, #30311, #16933, #19220, #14640, #19359, #4557, #12037 ) ) ;
#25152=( BOUNDED_CURVE ( )  B_SPLINE_CURVE ( 2, ( #1227, #22645, #17876, #30041, #8522, #18202, #27844, #15806, #25454, #10431, #3759, #23101, #20112, #27368, #5678, #15330, #3303, #12951, #28312, #9158, #16280, #30992, #2022, #6942, #13869, #8815, #23563, #1865, #30842, #16605, #18663, #6768, #18821, #25609, #1689, #16428, #23880, #21042, #11533, #18503, #6619, #21211, #25926, #28624, #30679, #28465, #11205, #4229, #14046, #26085, #4396, #30361, #23729, #11055, #20733, #8992, #11685, #28144, #21364, #6468, #8666, #26249, #9311, #18976, #20879, #4556, #14205, #18347, #27984, #6298, #15949, #3929, #30505, #13572, #23257, #1543, #16125, #25774, #4081, #13722, #23406 ),
 .UNSPECIFIED., .F., .T. ) 
 B_SPLINE_CURVE_WITH_KNOTS ( ( 3, 2, 2, 2, 2, 2, 2, 2, 2, 2, 2, 2, 2, 2, 2, 2, 2, 2, 2, 2, 2, 2, 2, 2, 2, 2, 2, 2, 2, 2, 2, 2, 2, 2, 2, 2, 2, 2, 2, 2, 3 ),
 ( 0.02979895253302125568, 0.03703703703703703498, 0.05555555555555555247, 0.07407407407407406996, 0.09259259259259258745, 0.1111111111111111049, 0.1296296296296295947, 0.1481481481481481399, 0.1666666666666666574, 0.1851851851851851749, 0.2037037037037036924, 0.2222222222222222099, 0.2407407407407407274, 0.2592592592592592449, 0.2777777777777777901, 0.2962962962962962798, 0.3148148148148147696, 0.3333333333333332593, 0.3518518518518518601, 0.3703703703703703498, 0.3888888888888889506, 0.4074074074074073293, 0.4259259259259259300, 0.4444444444444445308, 0.4629629629629629095, 0.4814814814814813992, 0.5000000000000001110, 0.5185185185185184897, 0.5370370370370370905, 0.5555555555555555802, 0.5740740740740740700, 0.5925925925925925597, 0.6111111111111111605, 0.6296296296296296502, 0.6481481481481481399, 0.6666666666666666297, 0.6851851851851852304, 0.7037037037037037202, 0.7222222222222222099, 0.7407407407407405886, 0.7410924888692722590 ),
 .UNSPECIFIED. ) 
 CURVE ( )  GEOMETRIC_REPRESENTATION_ITEM ( )  RATIONAL_B_SPLINE_CURVE ( ( 0.9362045903222155907, 0.9476351497648202171, 1.000000000000000000, 0.8660254037844387076, 1.000000000000000000, 0.8660254037844387076, 1.000000000000000000, 0.8660254037844387076, 1.000000000000000000, 0.8660254037844387076, 1.000000000000000000, 0.8660254037844387076, 1.000000000000000000, 0.8660254037844387076, 1.000000000000000000, 0.8660254037844387076, 1.000000000000000000, 0.8660254037844387076, 1.000000000000000000, 0.8660254037844387076, 1.000000000000000000, 0.8660254037844387076, 1.000000000000000000, 0.8660254037844387076, 1.000000000000000000, 0.8660254037844387076, 1.000000000000000000, 0.8660254037844387076, 1.000000000000000000, 0.8660254037844387076, 1.000000000000000000, 0.8660254037844387076, 1.000000000000000000, 0.8660254037844387076, 1.000000000000000000, 0.8660254037844387076, 1.000000000000000000, 0.8660254037844387076, 1.000000000000000000, 0.8660254037844387076, 1.000000000000000000, 0.8660254037844387076, 1.000000000000000000, 0.8660254037844387076, 1.000000000000000000, 0.8660254037844387076, 1.000000000000000000, 0.8660254037844387076, 1.000000000000000000, 0.8660254037844387076, 1.000000000000000000, 0.8660254037844387076, 1.000000000000000000, 0.8660254037844387076, 1.000000000000000000, 0.8660254037844387076, 1.000000000000000000, 0.8660254037844387076, 1.000000000000000000, 0.8660254037844387076, 1.000000000000000000, 0.8660254037844387076, 1.000000000000000000, 0.8660254037844387076, 1.000000000000000000, 0.8660254037844387076, 1.000000000000000000, 0.8660254037844387076, 1.000000000000000000, 0.8660254037844387076, 1.000000000000000000, 0.8660254037844387076, 1.000000000000000000, 0.8660254037844387076, 1.000000000000000000, 0.8660254037844387076, 1.000000000000000000, 0.8660254037844387076, 1.000000000000000000, 0.9974552330715619197, 0.9950071387796235456 ) ) 
 REPRESENTATION_ITEM ( '' )  );
#25161=CIRCLE ( 'NONE', #10009, 4.099999999999999645 ) ;
#25175=CARTESIAN_POINT ( 'NONE',  ( -55.67292740578360366, 1.073804522883522239, 3.225979517392336238 ) ) ;
#25181=CIRCLE ( 'NONE', #338, 2.100000000000000089 ) ;
#25183=MANIFOLD_SOLID_BREP ( 'Stock-MAS-683-1', #25140 ) ;
#25196=CARTESIAN_POINT ( 'NONE',  ( -54.49999999999997868, 3.206366378120874661, -1.671797828319853574 ) ) ;
#25221=( GEOMETRIC_REPRESENTATION_CONTEXT ( 3 ) GLOBAL_UNCERTAINTY_ASSIGNED_CONTEXT ( ( #24692 ) ) GLOBAL_UNIT_ASSIGNED_CONTEXT ( ( #5866, #15526, #18072 ) ) REPRESENTATION_CONTEXT ( 'NONE', 'WORKASPACE' ) );
#25235=DIRECTION ( 'NONE',  ( 0.000000000000000000, 0.2008964009354148039, -0.9796124928211139560 ) ) ;
#25236=VERTEX_POINT ( 'NONE', #28615 ) ;
#25243=CARTESIAN_POINT ( 'NONE',  ( -59.17292740578360366, -3.330682475591783653, -0.6830477631804104943 ) ) ;
#25255=DIRECTION ( 'NONE',  ( -1.000000000000000000, -3.054027077731387480E-16, 2.042479963029832083E-16 ) ) ;
#25285=ORIENTED_EDGE ( 'NONE', *, *, #9701, .T. ) ;
#25328=CARTESIAN_POINT ( 'NONE',  ( -59.54792740578360366, 3.330682475591789427, 0.6830477631804111605 ) ) ;
#25342=DIRECTION ( 'NONE',  ( 0.000000000000000000, -0.2008964009354147484, 0.9796124928211139560 ) ) ;
#25355=DIRECTION ( 'NONE',  ( 1.000000000000000000, 3.054025858079668409E-16, -2.042474015755241579E-16 ) ) ;
#25369=VERTEX_POINT ( 'NONE', #16529 ) ;
#25399=ORIENTED_EDGE ( 'NONE', *, *, #9839, .T. ) ;
#25409=CARTESIAN_POINT ( 'NONE',  ( -58.47099364905386665, -0.2309624077928895125, -3.875409454552786848 ) ) ;
#25428=VERTEX_POINT ( 'NONE', #31076 ) ;
#25432=CARTESIAN_POINT ( 'NONE',  ( -58.40835481156723574, -0.8699069336946632092, 4.241846523238430144 ) ) ;
#25440=LINE ( 'NONE', #22626, #3927 ) ;
#25454=CARTESIAN_POINT ( 'NONE',  ( -54.92292740578361077, 1.073804522883522239, 3.225979517392335794 ) ) ;
#25460=ORIENTED_EDGE ( 'NONE', *, *, #16689, .T. ) ;
#25473=CARTESIAN_POINT ( 'NONE',  ( -56.23542740578360366, -3.725040285533364859, 1.239922660687674982 ) ) ;
#25498=DIRECTION ( 'NONE',  ( 0.000000000000000000, 0.2008964009354147762, -0.9796124928211140670 ) ) ;
#25511=FACE_OUTER_BOUND ( 'NONE', #24454, .T. ) ;
#25525=DIRECTION ( 'NONE',  ( 1.000000000000000000, 3.054025858079668409E-16, -2.042474015755241579E-16 ) ) ;
#25536=DIRECTION ( 'NONE',  ( 1.000000000000000000, 3.054025858079668409E-16, -2.042474015755241579E-16 ) ) ;
#25558=AXIS2_PLACEMENT_3D ( 'NONE', #6724, #14634, #24148 ) ;
#25564=CYLINDRICAL_SURFACE ( 'NONE', #7944, 3.750000000000000444 ) ;
#25571=CIRCLE ( 'NONE', #18521, 4.099999999999999645 ) ;
#25573=DIRECTION ( 'NONE',  ( -2.614375865348240525E-16, 0.2008964009354147762, -0.9796124928211140670 ) ) ;
#25574=ORIENTED_EDGE ( 'NONE', *, *, #26278, .F. ) ;
#25578=EDGE_CURVE ( 'NONE', #10453, #7998, #17510, .T. ) ;
#25584=CARTESIAN_POINT ( 'NONE',  ( -59.22085481156723574, 1.184343223768590692, 3.558065644182727638 ) ) ;
#25598=CONICAL_SURFACE ( 'NONE', #30630, 1.625000000000000444, 0.04363323129985093030 ) ;
#25603=AXIS2_PLACEMENT_3D ( 'NONE', #7360, #21947, #24449 ) ;
#25609=CARTESIAN_POINT ( 'NONE',  ( -56.48542740578359656, 2.936324665650199783, 2.606018187048507517 ) ) ;
#25611=CARTESIAN_POINT ( 'NONE',  ( -56.87486116251334067, -1.737685414808513018, 3.471684241605566879 ) ) ;
#25632=DIRECTION ( 'NONE',  ( 1.000000000000000000, 3.054025858079668409E-16, -2.042474015755241579E-16 ) ) ;
#25636=CARTESIAN_POINT ( 'NONE',  ( -58.29792740578360366, -1.073804522883517132, -3.225979517392335350 ) ) ;
#25654=CARTESIAN_POINT ( 'NONE',  ( -55.15835481156724285, -3.238593381231841928, -2.874284765127023356 ) ) ;
#25660=ORIENTED_EDGE ( 'NONE', *, *, #24704, .T. ) ;
#25679=CARTESIAN_POINT ( 'NONE',  ( -71.49999999999998579, -1.395601618875910821E-15, 2.917180974979867506E-15 ) ) ;
#25687=VERTEX_POINT ( 'NONE', #12905 ) ;
#25688=ORIENTED_EDGE ( 'NONE', *, *, #19964, .F. ) ;
#25716=AXIS2_PLACEMENT_3D ( 'NONE', #24987, #29584, #5846 ) ;
#25717=DIRECTION ( 'NONE',  ( 1.000000000000000000, 3.054025858079668409E-16, -2.042474015755241579E-16 ) ) ;
#25733=FACE_OUTER_BOUND ( 'NONE', #15932, .T. ) ;
#25751=CARTESIAN_POINT ( 'NONE',  ( -59.34585481156723574, 3.673546848079181970, 0.7533615035078068400 ) ) ;
#25753=DIRECTION ( 'NONE',  ( 0.000000000000000000, -0.2008964009354148039, 0.9796124928211139560 ) ) ;
#25762=DIRECTION ( 'NONE',  ( -1.000000000000000000, -3.054025858079668409E-16, 2.042474015755241579E-16 ) ) ;
#25766=AXIS2_PLACEMENT_3D ( 'NONE', #20778, #28204, #25498 ) ;
#25774=CARTESIAN_POINT ( 'NONE',  ( -59.23542740578360366, -3.725040285533367523, 1.239922660687668543 ) ) ;
#25795=CARTESIAN_POINT ( 'NONE',  ( -57.23542740578360366, 2.936324665650207333, 2.606018187048499080 ) ) ;
#25830=ORIENTED_EDGE ( 'NONE', *, *, #17069, .F. ) ;
#25839=ORIENTED_EDGE ( 'NONE', *, *, #21949, .F. ) ;
#25846=EDGE_CURVE ( 'NONE', #22862, #15739, #2337, .T. ) ;
#25865=CARTESIAN_POINT ( 'NONE',  ( -61.04792740578359656, 3.330682475591789427, 0.6830477631804114935 ) ) ;
#25870=DIRECTION ( 'NONE',  ( 0.000000000000000000, -0.2008964009354162750, 0.9796124928211136229 ) ) ;
#25874=CARTESIAN_POINT ( 'NONE',  ( -67.99999999999995737, -3.266925685480207642E-16, 2.202315069465528948E-15 ) ) ;
#25876=DIRECTION ( 'NONE',  ( -1.000000000000000000, -3.054025858079668409E-16, 2.042474015755241579E-16 ) ) ;
#25878=DIRECTION ( 'NONE',  ( 0.000000000000000000, -0.2008964009354147484, 0.9796124928211139560 ) ) ;
#25880=ORIENTED_EDGE ( 'NONE', *, *, #18915, .F. ) ;
#25893=DIRECTION ( 'NONE',  ( 0.9990482215818580203, 0.008762977932702540121, -0.04273009679227964680 ) ) ;
#25897=ORIENTED_EDGE ( 'NONE', *, *, #11692, .T. ) ;
#25902=CARTESIAN_POINT ( 'NONE',  ( -57.84585481156723574, 3.673546848079182414, 0.7533615035078065070 ) ) ;
#25907=DIRECTION ( 'NONE',  ( 0.000000000000000000, 0.2008964009354147484, -0.9796124928211140670 ) ) ;
#25912=DIRECTION ( 'NONE',  ( 1.000000000000000000, 3.054025858079668409E-16, -2.042474015755241579E-16 ) ) ;
#25914=ADVANCED_FACE ( 'NONE', ( #30121 ), #23618, .T. ) ;
#25926=CARTESIAN_POINT ( 'NONE',  ( -57.04792740578359656, -2.256877952708267188, 2.542931754211920747 ) ) ;
#25935=ORIENTED_EDGE ( 'NONE', *, *, #6255, .F. ) ;
#25943=EDGE_CURVE ( 'NONE', #17250, #19589, #16100, .T. ) ;
#25949=CARTESIAN_POINT ( 'NONE',  ( -56.62499999999997158, 1.184343223768590470, 3.558065644182724974 ) ) ;
#25973=CARTESIAN_POINT ( 'NONE',  ( -69.22071067811863543, -0.4218824419643721901, 2.057186234924341939 ) ) ;
#25983=DIRECTION ( 'NONE',  ( -2.614375865348240525E-16, 0.2008964009354147762, -0.9796124928211140670 ) ) ;
#25987=CARTESIAN_POINT ( 'NONE',  ( 0.000000000000000000, 0.000000000000000000, 0.000000000000000000 ) ) ;
#25993=CARTESIAN_POINT ( 'NONE',  ( -60.54800159808252147, 0.7228413094357374336, -3.524724055549727897 ) ) ;
#25996=CIRCLE ( 'NONE', #24479, 4.849999999999999645 ) ;
#25999=CARTESIAN_POINT ( 'NONE',  ( -57.93749999999997158, -4.108500314926509134, 1.367561758111401016 ) ) ;
#26030=EDGE_CURVE ( 'NONE', #2983, #29251, #29824, .T. ) ;
#26034=CARTESIAN_POINT ( 'NONE',  ( -54.69184846062112371, 0.2309624077929086361, 3.875409454552791733 ) ) ;
#26045=CARTESIAN_POINT ( 'NONE',  ( -55.06249999999997158, -0.7533615035078029543, 3.673546848079176197 ) ) ;
#26051=EDGE_CURVE ( 'NONE', #11593, #11104, #16547, .T. ) ;
#26055=EDGE_CURVE ( 'NONE', #23943, #10453, #6410, .T. ) ;
#26057=CARTESIAN_POINT ( 'NONE',  ( -56.47085481156723574, 2.489203624310592389, -2.804704140674919355 ) ) ;
#26063=DIRECTION ( 'NONE',  ( -2.614375865348241018E-16, 0.2008964009354147762, -0.9796124928211140670 ) ) ;
#26084=VECTOR ( 'NONE', #18741, 1000.000000000000000 ) ;
#26085=CARTESIAN_POINT ( 'NONE',  ( -57.48542740578360366, 0.7887156198831770659, -3.845940847736172064 ) ) ;
#26087=CARTESIAN_POINT ( 'NONE',  ( -55.81249999999997868, -0.7533615035078013999, 3.673546848079176641 ) ) ;
#26098=ADVANCED_FACE ( 'NONE', ( #16038 ), #28142, .F. ) ;
#26108=CARTESIAN_POINT ( 'NONE',  ( -56.87499999999997158, 2.489203624310591056, -2.804704140674918023 ) ) ;
#26177=( BOUNDED_CURVE ( )  B_SPLINE_CURVE ( 2, ( #15584, #1158, #27763, #20195, #29825 ),
 .UNSPECIFIED., .F., .T. ) 
 B_SPLINE_CURVE_WITH_KNOTS ( ( 3, 2, 3 ),
 ( 0.000000000000000000, 0.01851851851851851749, 0.02777777777777778317 ),
 .UNSPECIFIED. ) 
 CURVE ( )  GEOMETRIC_REPRESENTATION_ITEM ( )  RATIONAL_B_SPLINE_CURVE ( ( 1.000000000000000000, 0.8660254037844387076, 1.000000000000000000, 0.9330127018922192983, 0.9330127018922194093 ) ) 
 REPRESENTATION_ITEM ( '' )  );
#26203=DIRECTION ( 'NONE',  ( 1.000000000000000000, 3.054025858079668409E-16, -2.042474015755241579E-16 ) ) ;
#26207=CARTESIAN_POINT ( 'NONE',  ( -57.22499999999997300, -0.8236752438351979677, 4.016411220566566520 ) ) ;
#26216=VERTEX_POINT ( 'NONE', #24556 ) ;
#26224=CARTESIAN_POINT ( 'NONE',  ( -55.29792740578360366, -1.073804522883516688, -3.225979517392336238 ) ) ;
#26234=DIRECTION ( 'NONE',  ( 0.000000000000000000, 0.2008964009354162750, -0.9796124928211136229 ) ) ;
#26246=EDGE_CURVE ( 'NONE', #2667, #11593, #25109, .T. ) ;
#26249=CARTESIAN_POINT ( 'NONE',  ( -58.23542740578360366, 0.7887156198831916099, -3.845940847736168511 ) ) ;
#26270=ORIENTED_EDGE ( 'NONE', *, *, #10566, .F. ) ;
#26271=CARTESIAN_POINT ( 'NONE',  ( -60.11042740578358945, -0.7887156198831607457, 3.845940847736174728 ) ) ;
#26278=EDGE_CURVE ( 'NONE', #15739, #20313, #13509, .T. ) ;
#26281=CARTESIAN_POINT ( 'NONE',  ( -57.27900635094606940, -1.737685414808519457, 3.471684241605561994 ) ) ;
#26289=AXIS2_PLACEMENT_3D ( 'NONE', #24859, #17431, #5710 ) ;
#26305=AXIS2_PLACEMENT_3D ( 'NONE', #5480, #1042, #27164 ) ;
#26357=CARTESIAN_POINT ( 'NONE',  ( -58.62499999999997158, -3.673546848079170424, -0.7533615035078236044 ) ) ;
#26378=CARTESIAN_POINT ( 'NONE',  ( -55.04792740578361077, 3.330682475591790315, 0.6830477631804101613 ) ) ;
#26402=CARTESIAN_POINT ( 'NONE',  ( -56.28335481156722864, 3.238593381231848145, 2.874284765127022467 ) ) ;
#26423=CARTESIAN_POINT ( 'NONE',  ( -54.49999999999997868, 3.673546848079181082, 0.7533615035078053968 ) ) ;
#26431=B_SPLINE_CURVE_WITH_KNOTS ( 'NONE', 3,
 ( #27336, #17364, #15301, #20809, #12759, #30440, #10987, #22437, #3853, #732, #24946, #3692, #18431, #13502, #5318, #20667, #10239, #23192 ),
 .UNSPECIFIED., .F., .F.,
 ( 4, 2, 2, 2, 2, 2, 2, 2, 4 ),
 ( 1.986428814944108226E-17, 0.0007541749550748564745, 0.001508349910149693216, 0.002262524865224529742, 0.003016699820299365616, 0.003770874775374201925, 0.004525049730449038667, 0.005279224685523875409, 0.006033399640598711283 ),
 .UNSPECIFIED. ) ;
#26437=CARTESIAN_POINT ( 'NONE',  ( -71.49999999999998579, 0.9743475445367603127, -4.751120590182400960 ) ) ;
#26443=LINE ( 'NONE', #1911, #19055 ) ;
#26469=DIRECTION ( 'NONE',  ( 2.581436205204234499E-16, -0.9796124928211140670, -0.2008964009354146651 ) ) ;
#26480=CARTESIAN_POINT ( 'NONE',  ( -60.44999999999996021, 1.979096954302128589E-15, 6.602471875703214707E-16 ) ) ;
#26487=ORIENTED_EDGE ( 'NONE', *, *, #13871, .F. ) ;
#26493=EDGE_LOOP ( 'NONE', ( #23920, #531, #10745, #2173 ) ) ;
#26514=EDGE_CURVE ( 'NONE', #9168, #23979, #9448, .T. ) ;
#26521=ORIENTED_EDGE ( 'NONE', *, *, #15831, .F. ) ;
#26526=CARTESIAN_POINT ( 'NONE',  ( -59.90835481156723574, -0.8699069336946634312, 4.241846523238430144 ) ) ;
#26536=ORIENTED_EDGE ( 'NONE', *, *, #22961, .T. ) ;
#26537=CIRCLE ( 'NONE', #11357, 0.04999999999999988481 ) ;
#26547=CARTESIAN_POINT ( 'NONE',  ( -56.22085481156723574, 1.184343223768591358, 3.558065644182726750 ) ) ;
#26550=EDGE_CURVE ( 'NONE', #13819, #11624, #5440, .T. ) ;
#26572=CARTESIAN_POINT ( 'NONE',  ( -58.62499999999997158, -3.673546848079174421, -0.7533615035078059519 ) ) ;
#26573=CARTESIAN_POINT ( 'NONE',  ( -57.68749999999996447, 0.7533615035078071731, -3.673546848079177085 ) ) ;
#26580=DIRECTION ( 'NONE',  ( -1.000000000000000000, -3.054025858079668409E-16, 2.042474015755241579E-16 ) ) ;
#26583=VERTEX_POINT ( 'NONE', #30727 ) ;
#26616=CARTESIAN_POINT ( 'NONE',  ( -56.31249999999997868, -3.238593381231836155, -2.874284765127025576 ) ) ;
#26648=ORIENTED_EDGE ( 'NONE', *, *, #22642, .F. ) ;
#26663=ORIENTED_EDGE ( 'NONE', *, *, #22943, .T. ) ;
#26680=CARTESIAN_POINT ( 'NONE',  ( -58.81249999999996447, -0.7533615035078081723, 3.673546848079176197 ) ) ;
#26684=DIRECTION ( 'NONE',  ( 0.000000000000000000, 0.2008964009354148039, -0.9796124928211139560 ) ) ;
#26688=DIRECTION ( 'NONE',  ( 0.000000000000000000, -0.2008964009354147484, 0.9796124928211139560 ) ) ;
#26702=CARTESIAN_POINT ( 'NONE',  ( -60.78335481156722864, 3.238593381231847257, 2.874284765127023356 ) ) ;
#26707=EDGE_LOOP ( 'NONE', ( #5832, #19200, #15759, #15028, #3479, #1, #27374, #14019, #21422, #6747, #8296, #25880, #10496, #26648, #29993, #31082, #5378 ) ) ;
#26727=AXIS2_PLACEMENT_3D ( 'NONE', #10960, #8725, #1005 ) ;
#26748=CARTESIAN_POINT ( 'NONE',  ( -60.68749999999996447, 0.8699069336946680941, -4.241846523238426592 ) ) ;
#26750=CARTESIAN_POINT ( 'NONE',  ( -60.54800159808252147, 1.949167012834402697E-15, 6.802637593289325421E-16 ) ) ;
#26751=COLOUR_RGB ( '', 0.66274510, 0.83137255, 0.94901961) ;
#26753=AXIS2_PLACEMENT_3D ( 'NONE', #614, #14570, #2545 ) ;
#26754=CARTESIAN_POINT ( 'NONE',  ( -54.49999999999997868, -3.745083032500879039, 0.1919715595446555012 ) ) ;
#26756=FACE_BOUND ( 'NONE', #15920, .T. ) ;
#26760=DIRECTION ( 'NONE',  ( 1.000000000000000000, 3.054025858079668409E-16, -2.042474015755241579E-16 ) ) ;
#26777=ORIENTED_EDGE ( 'NONE', *, *, #17984, .F. ) ;
#26779=CARTESIAN_POINT ( 'NONE',  ( -54.67292740578360366, -3.330682475591782765, -0.6830477631804114935 ) ) ;
#26782=ORIENTED_EDGE ( 'NONE', *, *, #16203, .T. ) ;
#26800=EDGE_LOOP ( 'NONE', ( #19958, #13234, #4245, #6906 ) ) ;
#26802=FACE_OUTER_BOUND ( 'NONE', #15611, .T. ) ;
#26816=EDGE_CURVE ( 'NONE', #29802, #5422, #21389, .T. ) ;
#26829=LINE ( 'NONE', #27131, #11945 ) ;
#26842=CARTESIAN_POINT ( 'NONE',  ( -56.04792740578360366, -1.073804522883516688, -3.225979517392335794 ) ) ;
#26849=VERTEX_POINT ( 'NONE', #3586 ) ;
#26855=FACE_OUTER_BOUND ( 'NONE', #6753, .T. ) ;
#26883=CARTESIAN_POINT ( 'NONE',  ( -59.06249999999997158, 4.108500314926511798, -1.367561758111406789 ) ) ;
#26886=CARTESIAN_POINT ( 'NONE',  ( -55.06249999999997158, -0.7533615035078029543, 3.673546848079176197 ) ) ;
#26888=CARTESIAN_POINT ( 'NONE',  ( -54.81249999999997868, -3.238593381231840151, -2.874284765127020691 ) ) ;
#26897=EDGE_CURVE ( 'NONE', #9415, #5317, #18601, .T. ) ;
#26906=EDGE_CURVE ( 'NONE', #18872, #26583, #30039, .T. ) ;
#26913=CARTESIAN_POINT ( 'NONE',  ( -57.53335481156722864, -4.108500314926509134, 1.367561758111407455 ) ) ;
#26917=CARTESIAN_POINT ( 'NONE',  ( -55.36042740578360366, -2.936324665650200672, -2.606018187048498191 ) ) ;
#26927=CARTESIAN_POINT ( 'NONE',  ( -67.99999999999995737, 0.5554785485864213168, -2.708628542650378890 ) ) ;
#26958=EDGE_LOOP ( 'NONE', ( #29847, #18448 ) ) ;
#26969=EDGE_CURVE ( 'NONE', #18051, #26216, #31111, .T. ) ;
#26975=CARTESIAN_POINT ( 'NONE',  ( -56.72499999999997300, 4.506217466977128439, 0.9241234443029089363 ) ) ;
#26977=DIRECTION ( 'NONE',  ( -2.581436205204234499E-16, 0.9796124928211140670, 0.2008964009354147762 ) ) ;
#26980=VERTEX_POINT ( 'NONE', #6900 ) ;
#26985=CARTESIAN_POINT ( 'NONE',  ( -57.67292740578359656, -3.330682475591783209, -0.6830477631804108274 ) ) ;
#27016=DIRECTION ( 'NONE',  ( 1.000000000000000000, 3.054025858079668409E-16, -2.042474015755241579E-16 ) ) ;
#27027=DIRECTION ( 'NONE',  ( 1.000000000000000000, 3.054025858079668409E-16, -2.042474015755241579E-16 ) ) ;
#27030=CARTESIAN_POINT ( 'NONE',  ( -60.06249999999996447, -3.238593381231840596, -2.874284765127020247 ) ) ;
#27032=CARTESIAN_POINT ( 'NONE',  ( -55.37499999999997868, 2.489203624310592389, -2.804704140674917134 ) ) ;
#27033=CARTESIAN_POINT ( 'NONE',  ( -54.49999999999995737, -3.717069605117153230, -0.3187059169208771303 ) ) ;
#27037=ADVANCED_FACE ( 'NONE', ( #7530, #29215 ), #17190, .T. ) ;
#27068=ORIENTED_EDGE ( 'NONE', *, *, #9550, .T. ) ;
#27076=ORIENTED_EDGE ( 'NONE', *, *, #26550, .T. ) ;
#27114=SURFACE_SIDE_STYLE ('',( #24889 ) ) ;
#27131=CARTESIAN_POINT ( 'NONE',  ( -67.99999999999995737, -0.6629581230868689667, 3.232721226309677842 ) ) ;
#27145=CIRCLE ( 'NONE', #13479, 0.05000000000000009298 ) ;
#27149=AXIS2_PLACEMENT_3D ( 'NONE', #15873, #20659, #27762 ) ;
#27153=CARTESIAN_POINT ( 'NONE',  ( -57.36042740578360366, 3.725040285533370632, -1.239922660687675871 ) ) ;
#27164=DIRECTION ( 'NONE',  ( 0.000000000000000000, -0.2008964009354143876, 0.9796124928211140670 ) ) ;
#27189=( BOUNDED_CURVE ( )  B_SPLINE_CURVE ( 2, ( #4606, #24392, #14411, #7295, #24245, #26913, #2850, #21735, #28840 ),
 .UNSPECIFIED., .F., .T. ) 
 B_SPLINE_CURVE_WITH_KNOTS ( ( 3, 2, 2, 2, 3 ),
 ( 0.4722222222222222099, 0.4814814814814814548, 0.5000000000000000000, 0.5185185185185184897, 0.5277777777777777901 ),
 .UNSPECIFIED. ) 
 CURVE ( )  GEOMETRIC_REPRESENTATION_ITEM ( )  RATIONAL_B_SPLINE_CURVE ( ( 0.9330127018922194093, 0.9330127018922194093, 1.000000000000000000, 0.8660254037844387076, 1.000000000000000000, 0.8660254037844387076, 1.000000000000000000, 0.9330127018922194093, 0.9330127018922194093 ) ) 
 REPRESENTATION_ITEM ( '' )  );
#27204=CARTESIAN_POINT ( 'NONE',  ( -57.12499999999997158, -3.673546848079173976, -0.7533615035078062849 ) ) ;
#27207=CARTESIAN_POINT ( 'NONE',  ( -55.06249999999997158, -0.7533615035078029543, 3.673546848079176197 ) ) ;
#27208=CARTESIAN_POINT ( 'NONE',  ( -59.30000000000042348, -2.541725022351402963, -2.757196748647571027 ) ) ;
#27209=FACE_OUTER_BOUND ( 'NONE', #22059, .T. ) ;
#27230=AXIS2_PLACEMENT_3D ( 'NONE', #21259, #30891, #6995 ) ;
#27233=CARTESIAN_POINT ( 'NONE',  ( -67.98046642889043767, -0.6631150920522017600, 3.233486639521210293 ) ) ;
#27252=AXIS2_PLACEMENT_3D ( 'NONE', #16846, #12092, #18756 ) ;
#27277=VERTEX_POINT ( 'NONE', #8739 ) ;
#27279=CIRCLE ( 'NONE', #25766, 4.835355339059328017 ) ;
#27305=EDGE_CURVE ( 'NONE', #3096, #18872, #6378, .T. ) ;
#27310=CARTESIAN_POINT ( 'NONE',  ( -58.36042740578360366, -2.936324665650201116, -2.606018187048497747 ) ) ;
#27316=ORIENTED_EDGE ( 'NONE', *, *, #13640, .T. ) ;
#27320=CARTESIAN_POINT ( 'NONE',  ( -58.24999999999997158, 3.673546848079177085, 0.7533615035078238265 ) ) ;
#27336=CARTESIAN_POINT ( 'NONE',  ( -59.29999999999997584, -2.208048483361063852, 2.585444235547710967 ) ) ;
#27357=ORIENTED_EDGE ( 'NONE', *, *, #26969, .F. ) ;
#27368=CARTESIAN_POINT ( 'NONE',  ( -55.23542740578361077, 0.7887156198831712928, -3.845940847736172952 ) ) ;
#27374=ORIENTED_EDGE ( 'NONE', *, *, #15150, .F. ) ;
#27391=FACE_OUTER_BOUND ( 'NONE', #2226, .T. ) ;
#27392=DIRECTION ( 'NONE',  ( 2.581436205204234006E-16, -0.9796124928211140670, -0.2008964009354148872 ) ) ;
#27394=CARTESIAN_POINT ( 'NONE',  ( -59.29999999999995453, -3.258916689102660857, -1.720755220692627097 ) ) ;
#27402=ADVANCED_FACE ( 'NONE', ( #10311 ), #10440, .T. ) ;
#27430=PRESENTATION_STYLE_ASSIGNMENT (( #522 ) ) ;
#27446=CARTESIAN_POINT ( 'NONE',  ( -71.49999999999998579, -0.9743475445367636434, 4.751120590182405401 ) ) ;
#27454=ORIENTED_EDGE ( 'NONE', *, *, #24354, .T. ) ;
#27457=CARTESIAN_POINT ( 'NONE',  ( -58.23542740578360366, 0.7887156198831662968, -3.845940847736174284 ) ) ;
#27497=DIRECTION ( 'NONE',  ( 0.000000000000000000, 0.2008964009354152203, -0.9796124928211138450 ) ) ;
#27502=DIRECTION ( 'NONE',  ( 0.000000000000000000, -0.2008964009354147484, 0.9796124928211140670 ) ) ;
#27513=CARTESIAN_POINT ( 'NONE',  ( -59.29999999999997584, -0.7533615035078030653, 3.673546848079178417 ) ) ;
#27520=DIRECTION ( 'NONE',  ( 2.581436205204234006E-16, -0.9796124928211140670, -0.2008964009354148872 ) ) ;
#27532=DIRECTION ( 'NONE',  ( 1.000000000000000000, 3.054025858079668409E-16, -2.042474015755241579E-16 ) ) ;
#27533=CARTESIAN_POINT ( 'NONE',  ( -57.48542740578361077, 0.7887156198831664078, -3.845940847736174284 ) ) ;
#27537=DIRECTION ( 'NONE',  ( -1.000000000000000000, -3.054025858079668409E-16, 2.042474015755241579E-16 ) ) ;
#27549=DIRECTION ( 'NONE',  ( -2.614375865348240525E-16, 0.2008964009354147207, -0.9796124928211138450 ) ) ;
#27556=CARTESIAN_POINT ( 'NONE',  ( -54.49999999999997868, 0.2900967345938421649, -3.387601494358211340 ) ) ;
#27558=ORIENTED_EDGE ( 'NONE', *, *, #15191, .F. ) ;
#27581=ORIENTED_EDGE ( 'NONE', *, *, #22376, .F. ) ;
#27586=ORIENTED_EDGE ( 'NONE', *, *, #515, .T. ) ;
#27615=CARTESIAN_POINT ( 'NONE',  ( -58.29792740578360366, -1.073804522883517132, -3.225979517392335350 ) ) ;
#27625=ORIENTED_EDGE ( 'NONE', *, *, #29123, .T. ) ;
#27635=CARTESIAN_POINT ( 'NONE',  ( -57.72085481156722864, 1.184343223768590914, 3.558065644182727194 ) ) ;
#27647=CARTESIAN_POINT ( 'NONE',  ( -58.72085481156723574, 2.489203624310592389, -2.804704140674918911 ) ) ;
#27658=CARTESIAN_POINT ( 'NONE',  ( -54.53335481156723574, -4.108500314926510022, 1.367561758111406789 ) ) ;
#27683=ORIENTED_EDGE ( 'NONE', *, *, #28217, .T. ) ;
#27692=CARTESIAN_POINT ( 'NONE',  ( -67.99999999999995737, -0.5554785485864222050, 2.708628542650383331 ) ) ;
#27709=CARTESIAN_POINT ( 'NONE',  ( -59.42292740578359656, 1.073804522883521351, 3.225979517392337126 ) ) ;
#27717=ORIENTED_EDGE ( 'NONE', *, *, #6112, .T. ) ;
#27744=DIRECTION ( 'NONE',  ( 2.581436205204234499E-16, -0.9796124928211140670, -0.2008964009354146651 ) ) ;
#27750=ORIENTED_EDGE ( 'NONE', *, *, #30930, .F. ) ;
#27753=ORIENTED_EDGE ( 'NONE', *, *, #8505, .F. ) ;
#27762=DIRECTION ( 'NONE',  ( 0.000000000000000000, -0.2008964009354148039, 0.9796124928211140670 ) ) ;
#27763=CARTESIAN_POINT ( 'NONE',  ( -54.62499999999997868, 2.489203624310591501, -2.804704140674918467 ) ) ;
#27766=CYLINDRICAL_SURFACE ( 'NONE', #11450, 3.750000000000000444 ) ;
#27822=CARTESIAN_POINT ( 'NONE',  ( -57.47085481156722864, -3.673546848079175753, -0.7533615035078066180 ) ) ;
#27844=CARTESIAN_POINT ( 'NONE',  ( -54.79792740578361077, -2.256877952708263191, 2.542931754211923856 ) ) ;
#27846=ADVANCED_FACE ( 'NONE', ( #5365 ), #7932, .T. ) ;
#27863=CARTESIAN_POINT ( 'NONE',  ( -56.29792740578360366, -2.256877952708263635, 2.542931754211924300 ) ) ;
#27873=CARTESIAN_POINT ( 'NONE',  ( -56.56249999999997158, -0.7533615035078050637, 3.673546848079176641 ) ) ;
#27893=( BOUNDED_CURVE ( )  B_SPLINE_CURVE ( 2, ( #4038, #26034, #4512, #23214, #23690, #4185, #1807, #30796, #9107 ),
 .UNSPECIFIED., .F., .T. ) 
 B_SPLINE_CURVE_WITH_KNOTS ( ( 3, 2, 2, 2, 3 ),
 ( 0.08333333333333332871, 0.09259259259259258745, 0.1111111111111111049, 0.1296296296296296224, 0.1388888888888888951 ),
 .UNSPECIFIED. ) 
 CURVE ( )  GEOMETRIC_REPRESENTATION_ITEM ( )  RATIONAL_B_SPLINE_CURVE ( ( 0.9330127018922194093, 0.9330127018922194093, 1.000000000000000000, 0.8660254037844387076, 1.000000000000000000, 0.8660254037844387076, 1.000000000000000000, 0.9330127018922191873, 0.9330127018922192983 ) ) 
 REPRESENTATION_ITEM ( '' )  );
#27895=ORIENTED_EDGE ( 'NONE', *, *, #399, .T. ) ;
#27928=DIRECTION ( 'NONE',  ( 2.614375865348240525E-16, -0.2008964009354147762, 0.9796124928211140670 ) ) ;
#27931=CARTESIAN_POINT ( 'NONE',  ( -59.29999999999997584, 2.330309927981285032E-15, 4.253626757584724400E-16 ) ) ;
#27937=CARTESIAN_POINT ( 'NONE',  ( -59.18749999999996447, 0.7533615035078157218, -3.673546848079175309 ) ) ;
#27950=CARTESIAN_POINT ( 'NONE',  ( -54.49999999999997868, 3.796242339859525868E-15, -5.550248518040434488E-16 ) ) ;
#27952=FACE_OUTER_BOUND ( 'NONE', #14290, .T. ) ;
#27962=CARTESIAN_POINT ( 'NONE',  ( -56.28335481156724285, 3.238593381231848145, 2.874284765127022467 ) ) ;
#27969=ORIENTED_EDGE ( 'NONE', *, *, #2726, .F. ) ;
#27980=AXIS2_PLACEMENT_3D ( 'NONE', #11097, #15230, #24875 ) ;
#27984=CARTESIAN_POINT ( 'NONE',  ( -58.67292740578360366, 1.073804522883500701, 3.225979517392344231 ) ) ;
#27986=CARTESIAN_POINT ( 'NONE',  ( -56.72085481156723574, -3.673546848079175753, -0.7533615035078068400 ) ) ;
#28004=VERTEX_POINT ( 'NONE', #27692 ) ;
#28005=CARTESIAN_POINT ( 'NONE',  ( -57.86042740578360366, -0.7887156198831604126, 3.845940847736174284 ) ) ;
#28010=( BOUNDED_CURVE ( )  B_SPLINE_CURVE ( 2, ( #9536, #21880, #14257, #12201, #21730 ),
 .UNSPECIFIED., .F., .T. ) 
 B_SPLINE_CURVE_WITH_KNOTS ( ( 3, 2, 3 ),
 ( 0.7500000000000000000, 0.7592592592592593004, 0.7708295755062543053 ),
 .UNSPECIFIED. ) 
 CURVE ( )  GEOMETRIC_REPRESENTATION_ITEM ( )  RATIONAL_B_SPLINE_CURVE ( ( 0.9330127018922194093, 0.9330127018922194093, 1.000000000000000000, 0.9162930638470145883, 0.9371858258165919331 ) ) 
 REPRESENTATION_ITEM ( '' )  );
#28034=CARTESIAN_POINT ( 'NONE',  ( -59.29999999999997584, 2.330309927981284638E-15, 4.253626757584726372E-16 ) ) ;
#28040=DIRECTION ( 'NONE',  ( -1.000000000000000000, -3.054025858079668409E-16, 2.042474015755241579E-16 ) ) ;
#28083=CIRCLE ( 'NONE', #1791, 4.600000000000000533 ) ;
#28094=DIRECTION ( 'NONE',  ( -2.581436205204234499E-16, 0.9796124928211140670, 0.2008964009354147762 ) ) ;
#28110=CARTESIAN_POINT ( 'NONE',  ( -56.72499999999997300, 3.116721586436802063E-15, -1.005743832985040150E-16 ) ) ;
#28119=CARTESIAN_POINT ( 'NONE',  ( -57.40835481156724285, -3.238593381231841928, -2.874284765127022023 ) ) ;
#28142=TOROIDAL_SURFACE ( 'NONE', #16002, 4.600000000000000533, 0.5000000000000013323 ) ;
#28144=CARTESIAN_POINT ( 'NONE',  ( -57.98542740578360366, 2.936324665650198007, 2.606018187048509294 ) ) ;
#28159=ORIENTED_EDGE ( 'NONE', *, *, #4744, .F. ) ;
#28163=DIRECTION ( 'NONE',  ( 0.7071067811865539010, -0.1420552074174017965, 0.6926906366088616540 ) ) ;
#28170=CARTESIAN_POINT ( 'NONE',  ( -55.92292740578360366, 2.256877952708269408, -2.542931754211925632 ) ) ;
#28173=SHAPE_DEFINITION_REPRESENTATION ( #28327, #3777 ) ;
#28204=DIRECTION ( 'NONE',  ( -1.000000000000000000, -3.054025858079668409E-16, 2.042474015755241579E-16 ) ) ;
#28217=EDGE_CURVE ( 'NONE', #9091, #7150, #19350, .T. ) ;
#28224=ORIENTED_EDGE ( 'NONE', *, *, #29700, .F. ) ;
#28231=DIRECTION ( 'NONE',  ( 0.000000000000000000, 0.2008964009354147762, -0.9796124928211140670 ) ) ;
#28239=DIRECTION ( 'NONE',  ( 0.000000000000000000, 0.2008964009354147484, -0.9796124928211138450 ) ) ;
#28242=ORIENTED_EDGE ( 'NONE', *, *, #9550, .F. ) ;
#28256=FACE_OUTER_BOUND ( 'NONE', #16311, .T. ) ;
#28273=DIRECTION ( 'NONE',  ( 0.000000000000000000, -0.2008964009354147484, 0.9796124928211138450 ) ) ;
#28275=CARTESIAN_POINT ( 'NONE',  ( -55.87499999999997158, 1.184343223768590025, 3.558065644182724974 ) ) ;
#28285=CARTESIAN_POINT ( 'NONE',  ( -55.90835481156724285, -3.238593381231841928, -2.874284765127022467 ) ) ;
#28286=AXIS2_PLACEMENT_3D ( 'NONE', #8485, #20533, #23053 ) ;
#28292=ORIENTED_EDGE ( 'NONE', *, *, #12745, .T. ) ;
#28312=CARTESIAN_POINT ( 'NONE',  ( -55.54792740578360366, -2.256877952708265411, 2.542931754211921191 ) ) ;
#28327=PRODUCT_DEFINITION_SHAPE ( 'NONE', 'NONE',  #6239 ) ;
#28332=FACE_OUTER_BOUND ( 'NONE', #8679, .T. ) ;
#28335=CARTESIAN_POINT ( 'NONE',  ( -54.68749999999998579, 0.8699069336946692044, -4.241846523238429256 ) ) ;
#28379=CARTESIAN_POINT ( 'NONE',  ( -57.37499999999997158, 1.184343223768581366, 3.558065644182728082 ) ) ;
#28384=EDGE_CURVE ( 'NONE', #26849, #236, #29187, .T. ) ;
#28406=ORIENTED_EDGE ( 'NONE', *, *, #19474, .T. ) ;
#28421=DIRECTION ( 'NONE',  ( -1.000000000000000000, -3.054025858079668409E-16, 2.042474015755241579E-16 ) ) ;
#28424=CARTESIAN_POINT ( 'NONE',  ( -57.99986116251333357, 1.737685414808516793, -3.471684241605569099 ) ) ;
#28441=CARTESIAN_POINT ( 'NONE',  ( -56.97085481156723574, 1.184343223768591136, 3.558065644182727194 ) ) ;
#28447=EDGE_LOOP ( 'NONE', ( #2024, #19874, #25460, #7382 ) ) ;
#28448=DIRECTION ( 'NONE',  ( 0.000000000000000000, 0.2008964009354147484, -0.9796124928211139560 ) ) ;
#28459=EDGE_CURVE ( 'NONE', #12772, #23943, #1133, .T. ) ;
#28465=CARTESIAN_POINT ( 'NONE',  ( -57.23542740578360366, 2.936324665650198895, 2.606018187048508850 ) ) ;
#28485=ORIENTED_EDGE ( 'NONE', *, *, #24721, .F. ) ;
#28486=CARTESIAN_POINT ( 'NONE',  ( -55.18749999999997158, 3.238593381231846369, 2.874284765127020691 ) ) ;
#28508=CARTESIAN_POINT ( 'NONE',  ( -57.28335481156723574, 0.7533615035078095046, -3.673546848079178861 ) ) ;
#28519=VERTEX_POINT ( 'NONE', #25973 ) ;
#28531=CARTESIAN_POINT ( 'NONE',  ( -67.98046642889043767, -3.207269654211098678E-16, 2.198325388322918801E-15 ) ) ;
#28538=CARTESIAN_POINT ( 'NONE',  ( -57.99999999999997158, -2.489203624310590612, 2.804704140674912693 ) ) ;
#28545=TOROIDAL_SURFACE ( 'NONE', #1229, 1.524417381223824197, 0.05000000000000000278 ) ;
#28550=EDGE_CURVE ( 'NONE', #17250, #14688, #9361, .T. ) ;
#28586=CARTESIAN_POINT ( 'NONE',  ( -55.93749999999997868, 3.238593381231842816, 2.874284765127024688 ) ) ;
#28594=ORIENTED_EDGE ( 'NONE', *, *, #2080, .F. ) ;
#28597=CARTESIAN_POINT ( 'NONE',  ( -54.73542740578361077, -3.725040285533364859, 1.239922660687674760 ) ) ;
#28607=FACE_OUTER_BOUND ( 'NONE', #28869, .T. ) ;
#28615=CARTESIAN_POINT ( 'NONE',  ( -56.67499999999996874, 0.9743475445367648646, -4.751120590182402736 ) ) ;
#28621=CARTESIAN_POINT ( 'NONE',  ( -56.67499999999996874, -0.9643027244899884387, 4.702139965541347166 ) ) ;
#28624=CARTESIAN_POINT ( 'NONE',  ( -57.11042740578360366, -0.7887156198831699605, 3.845940847736171619 ) ) ;
#28633=ORIENTED_EDGE ( 'NONE', *, *, #13438, .T. ) ;
#28641=ORIENTED_EDGE ( 'NONE', *, *, #26550, .F. ) ;
#28649=CARTESIAN_POINT ( 'NONE',  ( -60.42292740578359656, 2.256877952708268520, -2.542931754211924300 ) ) ;
#28654=CIRCLE ( 'NONE', #18033, 4.314644660940672338 ) ;
#28670=CARTESIAN_POINT ( 'NONE',  ( -55.37486116251335488, -1.737685414808514350, 3.471684241605565990 ) ) ;
#28671=DIRECTION ( 'NONE',  ( -1.000000000000000000, -3.054025858079668409E-16, 2.042474015755241579E-16 ) ) ;
#28690=CARTESIAN_POINT ( 'NONE',  ( -56.56249999999997158, -0.7533615035078050637, 3.673546848079176197 ) ) ;
#28753=CARTESIAN_POINT ( 'NONE',  ( -56.15400635094609072, 1.737685414808526341, -3.471684241605562438 ) ) ;
#28756=ORIENTED_EDGE ( 'NONE', *, *, #2460, .F. ) ;
#28763=CARTESIAN_POINT ( 'NONE',  ( -59.47085481156723574, 2.489203624310591945, -2.804704140674918911 ) ) ;
#28781=TOROIDAL_SURFACE ( 'NONE', #27252, 4.279289321881344144, 0.05000000000000000278 ) ;
#28790=EDGE_CURVE ( 'NONE', #9864, #14055, #11836, .T. ) ;
#28791=DIRECTION ( 'NONE',  ( -1.000000000000000000, -3.054025858079668409E-16, 2.042474015755241579E-16 ) ) ;
#28805=CARTESIAN_POINT ( 'NONE',  ( -69.19999999999998863, -0.4218824419643717460, 2.057186234924341939 ) ) ;
#28809=CARTESIAN_POINT ( 'NONE',  ( -56.18749999999997158, 0.8699069336946689823, -4.241846523238429256 ) ) ;
#28815=FACE_OUTER_BOUND ( 'NONE', #3005, .T. ) ;
#28816=EDGE_CURVE ( 'NONE', #7825, #76, #20635, .T. ) ;
#28840=CARTESIAN_POINT ( 'NONE',  ( -57.65835481156722864, -0.7533615035078039535, 3.673546848079178861 ) ) ;
#28848=EDGE_LOOP ( 'NONE', ( #7492, #210, #9099, #29336 ) ) ;
#28869=EDGE_LOOP ( 'NONE', ( #2287, #18610 ) ) ;
#28880=ORIENTED_EDGE ( 'NONE', *, *, #26055, .T. ) ;
#28893=CARTESIAN_POINT ( 'NONE',  ( -58.56249999999997868, -3.238593381231838819, -2.874284765127022023 ) ) ;
#28910=CARTESIAN_POINT ( 'NONE',  ( -60.47085481156722864, -3.673546848079176197, -0.7533615035078059519 ) ) ;
#28915=CARTESIAN_POINT ( 'NONE',  ( -59.29999999999997584, -0.7533615035078030653, 3.673546848079178417 ) ) ;
#28952=CARTESIAN_POINT ( 'NONE',  ( -56.43749999999997158, -4.108500314926507357, 1.367561758111406345 ) ) ;
#29001=ORIENTED_EDGE ( 'NONE', *, *, #18671, .T. ) ;
#29003=CARTESIAN_POINT ( 'NONE',  ( -67.97846802697301882, 0.6530782982312793861, -3.184545152421069947 ) ) ;
#29050=CIRCLE ( 'NONE', #13328, 3.075000000000000622 ) ;
#29054=DIRECTION ( 'NONE',  ( 0.000000000000000000, -0.2008964009354162750, 0.9796124928211136229 ) ) ;
#29063=CARTESIAN_POINT ( 'NONE',  ( -56.17292740578360366, -3.330682475591782765, -0.6830477631804111605 ) ) ;
#29077=FACE_OUTER_BOUND ( 'NONE', #12067, .T. ) ;
#29109=CARTESIAN_POINT ( 'NONE',  ( -59.87499999999997158, 2.489203624310590168, -2.804704140674917134 ) ) ;
#29112=CIRCLE ( 'NONE', #19517, 4.279289321881344144 ) ;
#29115=CARTESIAN_POINT ( 'NONE',  ( -54.87499999999997868, -3.673546848079173532, -0.7533615035078067290 ) ) ;
#29123=EDGE_CURVE ( 'NONE', #1074, #28519, #25181, .T. ) ;
#29124=CARTESIAN_POINT ( 'NONE',  ( -54.54999999999998295, 3.780972210569126836E-15, -5.448124817252668230E-16 ) ) ;
#29140=CONICAL_SURFACE ( 'NONE', #25603, 1.625000000000000444, 0.04363323129985093030 ) ;
#29144=TOROIDAL_SURFACE ( 'NONE', #4340, 3.648039984012787063, 0.05000000000000000278 ) ;
#29146=ORIENTED_EDGE ( 'NONE', *, *, #2080, .T. ) ;
#29187=CIRCLE ( 'NONE', #3399, 3.648039984012787507 ) ;
#29197=ORIENTED_EDGE ( 'NONE', *, *, #8505, .T. ) ;
#29203=EDGE_LOOP ( 'NONE', ( #30739, #20212, #14136, #20075 ) ) ;
#29210=AXIS2_PLACEMENT_3D ( 'NONE', #28621, #1863, #11684 ) ;
#29215=FACE_BOUND ( 'NONE', #21308, .T. ) ;
#29218=ORIENTED_EDGE ( 'NONE', *, *, #20261, .T. ) ;
#29223=CARTESIAN_POINT ( 'NONE',  ( -60.65835481156722864, -0.8699069336946635422, 4.241846523238430144 ) ) ;
#29231=ORIENTED_EDGE ( 'NONE', *, *, #5186, .T. ) ;
#29232=CARTESIAN_POINT ( 'NONE',  ( -57.22499999999997300, 2.964020293532818446E-15, 1.549317489258299684E-18 ) ) ;
#29237=ORIENTED_EDGE ( 'NONE', *, *, #18931, .T. ) ;
#29251=VERTEX_POINT ( 'NONE', #12375 ) ;
#29255=ORIENTED_EDGE ( 'NONE', *, *, #24314, .T. ) ;
#29271=CARTESIAN_POINT ( 'NONE',  ( -58.43749999999997158, 0.8699069336946684272, -4.241846523238428368 ) ) ;
#29277=CARTESIAN_POINT ( 'NONE',  ( -54.50000000000000000, -3.329534718049536046, -1.527735671238820148 ) ) ;
#29279=PLANE ( 'NONE',  #24988 ) ;
#29286=DIRECTION ( 'NONE',  ( 1.000000000000000000, 3.054025858079668409E-16, -2.042474015755241579E-16 ) ) ;
#29290=VECTOR ( 'NONE', #21409, 1000.000000000000000 ) ;
#29303=CARTESIAN_POINT ( 'NONE',  ( -55.17292740578361077, 2.256877952708269408, -2.542931754211925632 ) ) ;
#29306=CARTESIAN_POINT ( 'NONE',  ( -59.29999999999999005, -2.874490093629469278, -2.376013416532390732 ) ) ;
#29336=ORIENTED_EDGE ( 'NONE', *, *, #26246, .F. ) ;
#29367=CARTESIAN_POINT ( 'NONE',  ( -60.23542740578359656, 2.936324665650206889, 2.606018187048499524 ) ) ;
#29380=VERTEX_POINT ( 'NONE', #6664 ) ;
#29403=CARTESIAN_POINT ( 'NONE',  ( -60.24999999999997868, 2.040177471463716435E-15, 6.193977072552205884E-16 ) ) ;
#29405=EDGE_CURVE ( 'NONE', #5422, #25428, #28010, .T. ) ;
#29414=CARTESIAN_POINT ( 'NONE',  ( -59.93749999999997158, 0.8699069336946682052, -4.241846523238426592 ) ) ;
#29426=CARTESIAN_POINT ( 'NONE',  ( -56.87499999999997158, 2.489203624310596386, -2.804704140674913582 ) ) ;
#29431=ORIENTED_EDGE ( 'NONE', *, *, #7889, .T. ) ;
#29447=CARTESIAN_POINT ( 'NONE',  ( -59.29999999999996163, -3.060620570343238089, 1.662570173752615954 ) ) ;
#29458=AXIS2_PLACEMENT_3D ( 'NONE', #7039, #14616, #17008 ) ;
#29462=DIRECTION ( 'NONE',  ( -2.614375865348241018E-16, 0.2008964009354147762, -0.9796124928211140670 ) ) ;
#29490=CARTESIAN_POINT ( 'NONE',  ( -59.29999999999997584, -0.7533615035078030653, 3.673546848079178417 ) ) ;
#29508=CARTESIAN_POINT ( 'NONE',  ( -59.92292740578359656, -3.330682475591783653, -0.6830477631804103833 ) ) ;
#29536=( BOUNDED_CURVE ( )  B_SPLINE_CURVE ( 2, ( #3947, #12976, #18365, #1248, #18524, #10910, #13587, #6030, #23277 ),
 .UNSPECIFIED., .F., .T. ) 
 B_SPLINE_CURVE_WITH_KNOTS ( ( 3, 2, 2, 2, 3 ),
 ( 0.1944444444444444475, 0.2037037037037036924, 0.2222222222222222099, 0.2407407407407407274, 0.2500000000000000000 ),
 .UNSPECIFIED. ) 
 CURVE ( )  GEOMETRIC_REPRESENTATION_ITEM ( )  RATIONAL_B_SPLINE_CURVE ( ( 0.9330127018922192983, 0.9330127018922194093, 1.000000000000000000, 0.8660254037844387076, 1.000000000000000000, 0.8660254037844387076, 1.000000000000000000, 0.9330127018922191873, 0.9330127018922192983 ) ) 
 REPRESENTATION_ITEM ( '' )  );
#29538=TOROIDAL_SURFACE ( 'NONE', #15897, 4.800000000000000711, 0.05000000000000000278 ) ;
#29548=CARTESIAN_POINT ( 'NONE',  ( -54.34585481156724285, -1.184343223768585807, -3.558065644182726306 ) ) ;
#29560=CARTESIAN_POINT ( 'NONE',  ( -57.18749999999997158, -4.108500314926507357, 1.367561758111406345 ) ) ;
#29563=CARTESIAN_POINT ( 'NONE',  ( -54.50000000000001421, -1.699814003251586492, -3.091037575173824603 ) ) ;
#29564=CARTESIAN_POINT ( 'NONE',  ( -59.27326758270456253, -1.949102190723507100, -3.303506793698848476 ) ) ;
#29565=CARTESIAN_POINT ( 'NONE',  ( -71.44999999999998863, -1.380331489585512972E-15, 2.906968604901091669E-15 ) ) ;
#29576=CARTESIAN_POINT ( 'NONE',  ( -71.49999999999998579, -1.395601618875910821E-15, 2.917180974979867506E-15 ) ) ;
#29584=DIRECTION ( 'NONE',  ( 1.000000000000000000, 3.054025858079668409E-16, -2.042474015755241579E-16 ) ) ;
#29601=COLOUR_RGB ( '', 0.66274510, 0.83137255, 0.94901961) ;
#29621=CARTESIAN_POINT ( 'NONE',  ( -71.44999999999998863, -1.380331489585512972E-15, 2.906968604901091669E-15 ) ) ;
#29626=CYLINDRICAL_SURFACE ( 'NONE', #11289, 3.075000000000000622 ) ;
#29630=ORIENTED_EDGE ( 'NONE', *, *, #13138, .F. ) ;
#29631=CARTESIAN_POINT ( 'NONE',  ( -59.92928932188130631, 0.9643027244899926576, -4.702139965541346278 ) ) ;
#29670=DIRECTION ( 'NONE',  ( 0.000000000000000000, 0.2008964009354148039, -0.9796124928211139560 ) ) ;
#29681=CARTESIAN_POINT ( 'NONE',  ( -59.23542740578359656, -3.725040285533365747, 1.239922660687675871 ) ) ;
#29691=CARTESIAN_POINT ( 'NONE',  ( -58.06249999999996447, -0.7533615035078129463, 3.673546848079175309 ) ) ;
#29700=EDGE_CURVE ( 'NONE', #18051, #27277, #16560, .T. ) ;
#29704=VECTOR ( 'NONE', #25525, 1000.000000000000000 ) ;
#29722=CARTESIAN_POINT ( 'NONE',  ( -55.28335481156723574, -4.108500314926510022, 1.367561758111406789 ) ) ;
#29732=CARTESIAN_POINT ( 'NONE',  ( -59.37499999999997158, -3.673546848079174421, -0.7533615035078058408 ) ) ;
#29736=CARTESIAN_POINT ( 'NONE',  ( -54.49999999999997868, -2.351239121950967181, -2.690277294116418361 ) ) ;
#29761=DIRECTION ( 'NONE',  ( -2.581436205204234499E-16, 0.9796124928211140670, 0.2008964009354147762 ) ) ;
#29767=CARTESIAN_POINT ( 'NONE',  ( -54.79792740578361077, -2.256877952708263191, 2.542931754211923856 ) ) ;
#29787=CARTESIAN_POINT ( 'NONE',  ( -54.49999999999999289, 2.184125401144869194, -2.774890241360551624 ) ) ;
#29799=ORIENTED_EDGE ( 'NONE', *, *, #15215, .F. ) ;
#29802=VERTEX_POINT ( 'NONE', #19770 ) ;
#29807=ORIENTED_EDGE ( 'NONE', *, *, #30042, .F. ) ;
#29819=CARTESIAN_POINT ( 'NONE',  ( -57.22499999999997300, 0.9241234443029110457, -4.506217466977124886 ) ) ;
#29824=LINE ( 'NONE', #27446, #1859 ) ;
#29825=CARTESIAN_POINT ( 'NONE',  ( -54.68749999999997868, 0.7533615035078081723, -3.673546848079177973 ) ) ;
#29827=CARTESIAN_POINT ( 'NONE',  ( -55.81249999999997868, -0.7533615035078013999, 3.673546848079176641 ) ) ;
#29829=B_SPLINE_CURVE_WITH_KNOTS ( 'NONE', 3,
 ( #27556, #10634, #982, #22981, #5722, #10482, #29787, #13608, #20460, #8704, #25196, #23149, #1267, #5885, #6192, #17918, #18388, #6340 ),
 .UNSPECIFIED., .F., .F.,
 ( 4, 2, 2, 2, 2, 2, 2, 2, 4 ),
 ( 0.000000000000000000, 0.0007552462382147887140, 0.001510492476429577428, 0.002265738714644366034, 0.003020984952859154856, 0.003776231191073943678, 0.004531477429288733802, 0.005286723667503522191, 0.006041969905718312314 ),
 .UNSPECIFIED. ) ;
#29836=EDGE_LOOP ( 'NONE', ( #19080, #9062, #8264, #23824 ) ) ;
#29838=CARTESIAN_POINT ( 'NONE',  ( -59.36042740578360366, -0.7887156198831606346, 3.845940847736174284 ) ) ;
#29843=DIRECTION ( 'NONE',  ( 2.614375865348240525E-16, -0.2008964009354147762, 0.9796124928211140670 ) ) ;
#29844=VERTEX_POINT ( 'NONE', #3123 ) ;
#29847=ORIENTED_EDGE ( 'NONE', *, *, #4744, .T. ) ;
#29879=VERTEX_POINT ( 'NONE', #17232 ) ;
#29920=CARTESIAN_POINT ( 'NONE',  ( -58.92292740578360366, 2.256877952708268964, -2.542931754211924744 ) ) ;
#29922=DIRECTION ( 'NONE',  ( 0.000000000000000000, 0.2008964009354143876, -0.9796124928211140670 ) ) ;
#29928=EDGE_CURVE ( 'NONE', #24531, #8907, #12483, .T. ) ;
#29938=DIRECTION ( 'NONE',  ( 1.000000000000000000, 3.054025858079668409E-16, -2.042474015755241579E-16 ) ) ;
#29987=CARTESIAN_POINT ( 'NONE',  ( -59.73542740578360366, 0.7887156198831659637, -3.845940847736173840 ) ) ;
#29993=ORIENTED_EDGE ( 'NONE', *, *, #12654, .F. ) ;
#29995=ORIENTED_EDGE ( 'NONE', *, *, #10383, .F. ) ;
#30006=AXIS2_PLACEMENT_3D ( 'NONE', #24951, #27016, #10243 ) ;
#30009=CARTESIAN_POINT ( 'NONE',  ( -58.90835481156722864, -3.238593381231842816, -2.874284765127022023 ) ) ;
#30035=CARTESIAN_POINT ( 'NONE',  ( -59.92928932188130631, 0.9743475445367641985, -4.751120590182401848 ) ) ;
#30039=( BOUNDED_CURVE ( )  B_SPLINE_CURVE ( 2, ( #21478, #14174, #28275, #28586, #30633, #18788, #6588, #28753, #2465 ),
 .UNSPECIFIED., .F., .T. ) 
 B_SPLINE_CURVE_WITH_KNOTS ( ( 3, 2, 2, 2, 3 ),
 ( 0.1944444444444444475, 0.2037037037037036924, 0.2222222222222222099, 0.2407407407407407274, 0.2500000000000000000 ),
 .UNSPECIFIED. ) 
 CURVE ( )  GEOMETRIC_REPRESENTATION_ITEM ( )  RATIONAL_B_SPLINE_CURVE ( ( 0.9330127018922192983, 0.9330127018922194093, 1.000000000000000000, 0.8660254037844387076, 1.000000000000000000, 0.8660254037844387076, 1.000000000000000000, 0.9330127018922191873, 0.9330127018922192983 ) ) 
 REPRESENTATION_ITEM ( '' )  );
#30041=CARTESIAN_POINT ( 'NONE',  ( -54.61042740578361077, -2.936324665650201116, -2.606018187048499080 ) ) ;
#30042=EDGE_CURVE ( 'NONE', #25236, #7825, #856, .T. ) ;
#30056=CARTESIAN_POINT ( 'NONE',  ( -59.29999999999997584, 2.330309927981285032E-15, 4.253626757584724400E-16 ) ) ;
#30059=DIRECTION ( 'NONE',  ( 0.000000000000000000, -0.2008964009354162750, 0.9796124928211136229 ) ) ;
#30065=CARTESIAN_POINT ( 'NONE',  ( -55.86042740578360366, 3.725040285533370632, -1.239922660687676315 ) ) ;
#30077=CYLINDRICAL_SURFACE ( 'NONE', #4392, 3.750000000000000444 ) ;
#30088=ORIENTED_EDGE ( 'NONE', *, *, #6824, .F. ) ;
#30121=FACE_OUTER_BOUND ( 'NONE', #24483, .T. ) ;
#30156=FACE_OUTER_BOUND ( 'NONE', #1039, .T. ) ;
#30174=CARTESIAN_POINT ( 'NONE',  ( -58.84585481156723574, -1.184343223768586473, -3.558065644182725418 ) ) ;
#30184=CARTESIAN_POINT ( 'NONE',  ( -57.22085481156723574, 2.489203624310592389, -2.804704140674919355 ) ) ;
#30220=EDGE_LOOP ( 'NONE', ( #28756, #30309, #24667, #27581 ) ) ;
#30226=DIRECTION ( 'NONE',  ( 1.000000000000000000, 3.054025858079668409E-16, -2.042474015755241579E-16 ) ) ;
#30227=ORIENTED_EDGE ( 'NONE', *, *, #20143, .T. ) ;
#30233=CARTESIAN_POINT ( 'NONE',  ( -56.61042740578360366, 3.725040285533371076, -1.239922660687675871 ) ) ;
#30247=ADVANCED_FACE ( 'NONE', ( #12580 ), #3239, .F. ) ;
#30268=CYLINDRICAL_SURFACE ( 'NONE', #18917, 4.849999999999999645 ) ;
#30280=CARTESIAN_POINT ( 'NONE',  ( -59.29999999999997584, 0.7533615035078071731, -3.673546848079177085 ) ) ;
#30288=CARTESIAN_POINT ( 'NONE',  ( -54.49999999999997868, 4.751120590182407177, 0.9743475445367620891 ) ) ;
#30309=ORIENTED_EDGE ( 'NONE', *, *, #20722, .T. ) ;
#30311=ADVANCED_FACE ( 'NONE', ( #28332 ), #15050, .T. ) ;
#30314=DIRECTION ( 'NONE',  ( 1.000000000000000000, 3.054025858079668409E-16, -2.042474015755241579E-16 ) ) ;
#30336=AXIS2_PLACEMENT_3D ( 'NONE', #5304, #20830, #25878 ) ;
#30340=CARTESIAN_POINT ( 'NONE',  ( -59.09585481156723574, -2.489203624310587504, 2.804704140674918911 ) ) ;
#30361=CARTESIAN_POINT ( 'NONE',  ( -57.61042740578359656, -2.936324665650192234, -2.606018187048508850 ) ) ;
#30362=CARTESIAN_POINT ( 'NONE',  ( -56.65835481156722864, -3.238593381231841928, -2.874284765127022467 ) ) ;
#30377=ORIENTED_EDGE ( 'NONE', *, *, #16789, .T. ) ;
#30384=CARTESIAN_POINT ( 'NONE',  ( -57.67292740578359656, -3.330682475591783209, -0.6830477631804108274 ) ) ;
#30414=DIRECTION ( 'NONE',  ( 0.000000000000000000, 0.2008964009354141933, -0.9796124928211140670 ) ) ;
#30426=AXIS2_PLACEMENT_3D ( 'NONE', #4811, #2128, #9739 ) ;
#30433=DIRECTION ( 'NONE',  ( 2.614381936396368743E-16, -0.2008964009354147762, 0.9796124928211139560 ) ) ;
#30440=CARTESIAN_POINT ( 'NONE',  ( -59.29999999999998295, -0.6915043170233550196, 3.445813225535238278 ) ) ;
#30485=CARTESIAN_POINT ( 'NONE',  ( -57.78335481156724285, 3.238593381231847257, 2.874284765127022911 ) ) ;
#30502=CONICAL_SURFACE ( 'NONE', #13287, 4.299999999999998934, 0.7853981633974466137 ) ;
#30505=CARTESIAN_POINT ( 'NONE',  ( -58.92292740578360366, 2.256877952708275625, -2.542931754211918527 ) ) ;
#30517=DIRECTION ( 'NONE',  ( 0.000000000000000000, -0.2008964009354147484, 0.9796124928211138450 ) ) ;
#30528=CARTESIAN_POINT ( 'NONE',  ( -56.36042740578360366, -0.7887156198831599685, 3.845940847736173840 ) ) ;
#30538=ADVANCED_FACE ( 'NONE', ( #15476 ), #18619, .F. ) ;
#30545=DIRECTION ( 'NONE',  ( 0.000000000000000000, 0.2008964009354148039, -0.9796124928211139560 ) ) ;
#30562=LINE ( 'NONE', #8870, #3723 ) ;
#30564=CIRCLE ( 'NONE', #24492, 1.524417381223824197 ) ;
#30586=CARTESIAN_POINT ( 'NONE',  ( -58.06249999999996447, -0.7533615035078129463, 3.673546848079175309 ) ) ;
#30597=DIRECTION ( 'NONE',  ( -1.000000000000000000, -3.054025858079668409E-16, 2.042474015755241579E-16 ) ) ;
#30598=DIRECTION ( 'NONE',  ( 0.000000000000000000, -0.2008964009354162750, 0.9796124928211136229 ) ) ;
#30604=EDGE_LOOP ( 'NONE', ( #29630, #13167, #23427 ) ) ;
#30615=CARTESIAN_POINT ( 'NONE',  ( -59.92928932188130631, 2.138123341857387114E-15, 5.538933845919563674E-16 ) ) ;
#30626=CARTESIAN_POINT ( 'NONE',  ( -59.29999999999997584, 2.330309927981285032E-15, 4.253626757584724400E-16 ) ) ;
#30630=AXIS2_PLACEMENT_3D ( 'NONE', #7179, #13835, #21763 ) ;
#30633=CARTESIAN_POINT ( 'NONE',  ( -55.99999999999997868, 3.673546848079180638, 0.7533615035078075062 ) ) ;
#30649=CARTESIAN_POINT ( 'NONE',  ( -58.53335481156722864, 3.238593381231847257, 2.874284765127022911 ) ) ;
#30661=ORIENTED_EDGE ( 'NONE', *, *, #8570, .F. ) ;
#30663=TOROIDAL_SURFACE ( 'NONE', #18499, 3.648039984012787063, 0.05000000000000000278 ) ;
#30679=CARTESIAN_POINT ( 'NONE',  ( -57.17292740578359656, 1.073804522883514023, 3.225979517392339346 ) ) ;
#30690=LINE ( 'NONE', #6015, #23429 ) ;
#30703=CARTESIAN_POINT ( 'NONE',  ( -59.92928932188130631, 2.138123341857387114E-15, 5.538933845919563674E-16 ) ) ;
#30707=CARTESIAN_POINT ( 'NONE',  ( -55.56249999999997158, -3.238593381231840151, -2.874284765127021579 ) ) ;
#30713=EDGE_CURVE ( 'NONE', #236, #26849, #4947, .T. ) ;
#30727=CARTESIAN_POINT ( 'NONE',  ( -56.18749999999997868, 0.7533615035078126132, -3.673546848079176641 ) ) ;
#30739=ORIENTED_EDGE ( 'NONE', *, *, #29928, .T. ) ;
#30761=CARTESIAN_POINT ( 'NONE',  ( -57.72099364905386665, -0.2309624077928972563, -3.875409454552788624 ) ) ;
#30796=CARTESIAN_POINT ( 'NONE',  ( -54.99986116251336199, 1.737685414808520790, -3.471684241605567323 ) ) ;
#30800=DIRECTION ( 'NONE',  ( 2.614381936396368743E-16, -0.2008964009354147762, 0.9796124928211139560 ) ) ;
#30805=FACE_OUTER_BOUND ( 'NONE', #1115, .T. ) ;
#30810=ORIENTED_EDGE ( 'NONE', *, *, #22402, .T. ) ;
#30817=CARTESIAN_POINT ( 'NONE',  ( -55.72085481156724285, 2.489203624310592833, -2.804704140674919799 ) ) ;
#30842=CARTESIAN_POINT ( 'NONE',  ( -56.17292740578360366, -3.330682475591780989, -0.6830477631804185989 ) ) ;
#30865=CARTESIAN_POINT ( 'NONE',  ( -55.31249999999998579, 4.108500314926513575, -1.367561758111407899 ) ) ;
#30891=DIRECTION ( 'NONE',  ( -1.000000000000000000, -3.054025858079668409E-16, 2.042474015755241579E-16 ) ) ;
#30920=CARTESIAN_POINT ( 'NONE',  ( -57.74999999999997158, -1.184343223768574260, -3.558065644182727638 ) ) ;
#30930=EDGE_CURVE ( 'NONE', #9415, #6633, #11532, .T. ) ;
#30933=ORIENTED_EDGE ( 'NONE', *, *, #28459, .F. ) ;
#30950=CARTESIAN_POINT ( 'NONE',  ( -58.77900635094606940, -1.737685414808524564, 3.471684241605558885 ) ) ;
#30970=CARTESIAN_POINT ( 'NONE',  ( -60.15835481156723574, 4.108500314926515351, -1.367561758111407455 ) ) ;
#30979=DIRECTION ( 'NONE',  ( 0.000000000000000000, 0.2008964009354148039, -0.9796124928211140670 ) ) ;
#30992=CARTESIAN_POINT ( 'NONE',  ( -55.73542740578360366, 2.936324665650202892, 2.606018187048502188 ) ) ;
#31001=VERTEX_POINT ( 'NONE', #2448 ) ;
#31002=DIRECTION ( 'NONE',  ( 0.000000000000000000, -0.2008964009354147762, 0.9796124928211140670 ) ) ;
#31010=CARTESIAN_POINT ( 'NONE',  ( -59.67292740578360366, 2.256877952708268964, -2.542931754211924744 ) ) ;
#31026=CARTESIAN_POINT ( 'NONE',  ( -55.34585481156723574, -2.489203624310586616, 2.804704140674918023 ) ) ;
#31033=ORIENTED_EDGE ( 'NONE', *, *, #28550, .F. ) ;
#31053=AXIS2_PLACEMENT_3D ( 'NONE', #17586, #29761, #30059 ) ;
#31057=DIRECTION ( 'NONE',  ( 1.000000000000000000, 3.054025858079668409E-16, -2.042474015755241579E-16 ) ) ;
#31070=AXIS2_PLACEMENT_3D ( 'NONE', #22414, #12423, #29843 ) ;
#31076=CARTESIAN_POINT ( 'NONE',  ( -59.29999999999997584, 3.111192537532289304, 2.093557019620777115 ) ) ;
#31082=ORIENTED_EDGE ( 'NONE', *, *, #26514, .F. ) ;
#31097=CARTESIAN_POINT ( 'NONE',  ( -58.74999999999997158, -2.489203624310601715, 2.804704140674903368 ) ) ;
#31100=CIRCLE ( 'NONE', #21010, 0.04999999999999989175 ) ;
#31105=DIRECTION ( 'NONE',  ( -2.614375865348240525E-16, 0.2008964009354147762, -0.9796124928211140670 ) ) ;
#31111=LINE ( 'NONE', #16247, #13028 ) ;
#31120=CARTESIAN_POINT ( 'NONE',  ( -55.11042740578361077, 3.725040285533371076, -1.239922660687676315 ) ) ;
#31147=AXIS2_PLACEMENT_3D ( 'NONE', #29124, #26760, #15495 ) ;
#31157=CIRCLE ( 'NONE', #11957, 4.849999999999999645 ) ;
#31175=CARTESIAN_POINT ( 'NONE',  ( -55.49999999999997868, -1.184343223768585140, -3.558065644182724085 ) ) ;
#31200=AXIS2_PLACEMENT_3D ( 'NONE', #6042, #20453, #27549 ) ;
#31206=TOROIDAL_SURFACE ( 'NONE', #3895, 4.600000000000000533, 0.5000000000000013323 ) ;
#31219=VECTOR ( 'NONE', #27532, 1000.000000000000000 ) ;
#31235=CARTESIAN_POINT ( 'NONE',  ( -58.15835481156722864, -3.238593381231842816, -2.874284765127022023 ) ) ;
#31236=CARTESIAN_POINT ( 'NONE',  ( -54.49999999999997868, 3.796242339859525868E-15, -5.550248518040434488E-16 ) ) ;
#31246=APPLICATION_CONTEXT ( 'automotive_design' ) ;
#31251=CARTESIAN_POINT ( 'NONE',  ( -59.15400635094607651, 1.737685414808532780, -3.471684241605560661 ) ) ;
#31277=DIRECTION ( 'NONE',  ( 0.000000000000000000, -0.2008964009354162750, 0.9796124928211136229 ) ) ;
#31280=AXIS2_PLACEMENT_3D ( 'NONE', #19654, #4914, #12335 ) ;
#31287=CARTESIAN_POINT ( 'NONE',  ( -56.73542740578360366, 0.7887156198831665188, -3.845940847736174284 ) ) ;
#31303=TOROIDAL_SURFACE ( 'NONE', #11577, 2.050000000000000266, 0.05000000000000000278 ) ;
#31309=ADVANCED_FACE ( 'NONE', ( #5745 ), #6363, .F. ) ;
#31310=VECTOR ( 'NONE', #4897, 1000.000000000000114 ) ;
#31321=DIRECTION ( 'NONE',  ( -1.000000000000000000, -3.054025858079668409E-16, 2.042474015755241579E-16 ) ) ;
ENDSEC;
END-ISO-10303-21;
